ISO-10303-21;
HEADER;
/* Generated by software containing ST-Developer
 * from STEP Tools, Inc. (www.steptools.com) 
 */

FILE_DESCRIPTION(
/* description */ ('XY cross-slide table'),
/* implementation_level */ '2;1');

FILE_NAME(
/* name */ 'Flanged lead nut (1).step',
/* time_stamp */ '2026-10-28T03:22:46-07:00',
/* author */ (''),
/* organization */ (''),
/* preprocessor_version */ 'ST-DEVELOPER v20.2',
/* originating_system */ 'Autodesk Translation Framework v15.17.0.0',
/* authorisation */ '');

FILE_SCHEMA (('AUTOMOTIVE_DESIGN { 1 0 10303 214 3 1 1 }'));
ENDSEC;

DATA;
#10=MECHANICAL_DESIGN_GEOMETRIC_PRESENTATION_REPRESENTATION('',(#1770),#62984);
#15=B_SPLINE_SURFACE_WITH_KNOTS('',3,3,((#51310,#51311,#51312,#51313,#51314,
#51315,#51316,#51317,#51318,#51319,#51320,#51321,#51322,#51323,#51324,#51325,
#51326,#51327,#51328,#51329,#51330,#51331,#51332,#51333,#51334,#51335,#51336,
#51337,#51338,#51339,#51340,#51341,#51342,#51343,#51344,#51345,#51346,#51347,
#51348,#51349,#51350,#51351,#51352,#51353,#51354,#51355,#51356,#51357,#51358,
#51359,#51360,#51361,#51362,#51363,#51364,#51365,#51366,#51367,#51368,#51369,
#51370,#51371,#51372,#51373,#51374,#51375,#51376,#51377,#51378,#51379,#51380,
#51381,#51382,#51383,#51384,#51385,#51386,#51387,#51388,#51389,#51390,#51391,
#51392,#51393,#51394,#51395,#51396,#51397,#51398,#51399,#51400,#51401,#51402,
#51403,#51404,#51405,#51406,#51407,#51408,#51409,#51410,#51411,#51412,#51413,
#51414,#51415,#51416,#51417,#51418,#51419,#51420,#51421,#51422,#51423,#51424),
(#51425,#51426,#51427,#51428,#51429,#51430,#51431,#51432,#51433,#51434,
#51435,#51436,#51437,#51438,#51439,#51440,#51441,#51442,#51443,#51444,#51445,
#51446,#51447,#51448,#51449,#51450,#51451,#51452,#51453,#51454,#51455,#51456,
#51457,#51458,#51459,#51460,#51461,#51462,#51463,#51464,#51465,#51466,#51467,
#51468,#51469,#51470,#51471,#51472,#51473,#51474,#51475,#51476,#51477,#51478,
#51479,#51480,#51481,#51482,#51483,#51484,#51485,#51486,#51487,#51488,#51489,
#51490,#51491,#51492,#51493,#51494,#51495,#51496,#51497,#51498,#51499,#51500,
#51501,#51502,#51503,#51504,#51505,#51506,#51507,#51508,#51509,#51510,#51511,
#51512,#51513,#51514,#51515,#51516,#51517,#51518,#51519,#51520,#51521,#51522,
#51523,#51524,#51525,#51526,#51527,#51528,#51529,#51530,#51531,#51532,#51533,
#51534,#51535,#51536,#51537,#51538,#51539),(#51540,#51541,#51542,#51543,
#51544,#51545,#51546,#51547,#51548,#51549,#51550,#51551,#51552,#51553,#51554,
#51555,#51556,#51557,#51558,#51559,#51560,#51561,#51562,#51563,#51564,#51565,
#51566,#51567,#51568,#51569,#51570,#51571,#51572,#51573,#51574,#51575,#51576,
#51577,#51578,#51579,#51580,#51581,#51582,#51583,#51584,#51585,#51586,#51587,
#51588,#51589,#51590,#51591,#51592,#51593,#51594,#51595,#51596,#51597,#51598,
#51599,#51600,#51601,#51602,#51603,#51604,#51605,#51606,#51607,#51608,#51609,
#51610,#51611,#51612,#51613,#51614,#51615,#51616,#51617,#51618,#51619,#51620,
#51621,#51622,#51623,#51624,#51625,#51626,#51627,#51628,#51629,#51630,#51631,
#51632,#51633,#51634,#51635,#51636,#51637,#51638,#51639,#51640,#51641,#51642,
#51643,#51644,#51645,#51646,#51647,#51648,#51649,#51650,#51651,#51652,#51653,
#51654),(#51655,#51656,#51657,#51658,#51659,#51660,#51661,#51662,#51663,
#51664,#51665,#51666,#51667,#51668,#51669,#51670,#51671,#51672,#51673,#51674,
#51675,#51676,#51677,#51678,#51679,#51680,#51681,#51682,#51683,#51684,#51685,
#51686,#51687,#51688,#51689,#51690,#51691,#51692,#51693,#51694,#51695,#51696,
#51697,#51698,#51699,#51700,#51701,#51702,#51703,#51704,#51705,#51706,#51707,
#51708,#51709,#51710,#51711,#51712,#51713,#51714,#51715,#51716,#51717,#51718,
#51719,#51720,#51721,#51722,#51723,#51724,#51725,#51726,#51727,#51728,#51729,
#51730,#51731,#51732,#51733,#51734,#51735,#51736,#51737,#51738,#51739,#51740,
#51741,#51742,#51743,#51744,#51745,#51746,#51747,#51748,#51749,#51750,#51751,
#51752,#51753,#51754,#51755,#51756,#51757,#51758,#51759,#51760,#51761,#51762,
#51763,#51764,#51765,#51766,#51767,#51768,#51769)),.UNSPECIFIED.,.F.,.F.,
 .F.,(4,4),(4,1,1,1,1,1,1,1,1,1,1,1,1,1,1,1,1,1,1,1,1,1,1,1,1,1,1,1,1,1,
1,1,1,1,1,1,1,1,1,1,1,1,1,1,1,1,1,1,1,1,1,1,1,1,1,1,1,1,1,1,1,1,1,1,1,1,
1,1,1,1,1,1,1,1,1,1,1,1,1,1,1,1,1,1,1,1,1,1,1,1,1,1,1,1,1,1,1,1,1,1,1,1,
1,1,1,1,1,1,1,1,1,1,4),(0.,0.173020531651036),(12.1475814751569,12.6421543672732,
13.1367272593894,13.6313001515056,14.1258730436219,14.6204459357381,15.1150188278544,
15.6095917199706,16.1041646120869,16.5987375042031,17.0933103963194,17.5878832884356,
18.0824561805519,18.5770290726681,19.0716019647843,19.5661748569006,20.0607477490168,
20.5553206411331,21.0498935332493,21.5444664253656,22.0390393174818,22.5336122095981,
23.0281851017143,23.5227579938306,24.0173308859468,24.511903778063,25.0064766701793,
25.5010495622955,25.9956224544118,26.490195346528,26.9847682386443,27.4793411307605,
27.9739140228768,28.468486914993,28.9630598071093,29.4576326992255,29.9522055913417,
30.446778483458,30.9413513755742,31.4359242676905,31.9304971598067,32.425070051923,
32.9196429440392,33.4142158361555,33.9087887282717,34.403361620388,34.8979345125042,
35.3925074046204,35.8870802967367,36.3816531888529,36.8762260809692,37.3707989730854,
37.8653718652017,38.3599447573179,38.8545176494342,39.3490905415504,39.8436634336667,
40.3382363257829,40.8328092178991,41.3273821100154,41.8219550021316,42.3165278942479,
42.8111007863641,43.3056736784804,43.8002465705966,44.2948194627129,44.7893923548291,
45.2839652469454,45.7785381390616,46.2731110311778,46.7676839232941,47.2622568154103,
47.7568297075266,48.2514025996428,48.7459754917591,49.2405483838753,49.7351212759916,
50.2296941681078,50.7242670602241,51.2188399523403,51.7134128444565,52.2079857365728,
52.702558628689,53.1971315208053,53.6917044129215,54.1862773050378,54.680850197154,
55.1754230892703,55.6699959813865,56.1645688735028,56.659141765619,57.1537146577353,
57.6482875498515,58.1428604419677,58.637433334084,59.1320062262002,59.6265791183165,
60.1211520104327,60.615724902549,61.1102977946652,61.6048706867815,62.0994435788977,
62.5940164710139,63.0885893631302,63.5831622552464,64.0777351473627,64.5723080394789,
65.0668809315952,65.5614538237114,66.0560267158277,66.5505996079439,67.0451725000601,
67.5397453921764),.UNSPECIFIED.);
#16=B_SPLINE_SURFACE_WITH_KNOTS('',3,3,((#51869,#51870,#51871,#51872,#51873,
#51874,#51875,#51876,#51877,#51878,#51879,#51880,#51881,#51882,#51883,#51884,
#51885,#51886,#51887,#51888,#51889,#51890,#51891,#51892,#51893,#51894,#51895,
#51896,#51897,#51898,#51899,#51900,#51901,#51902,#51903,#51904,#51905,#51906,
#51907,#51908,#51909,#51910,#51911,#51912,#51913,#51914,#51915,#51916,#51917,
#51918,#51919,#51920,#51921,#51922,#51923,#51924,#51925,#51926,#51927,#51928,
#51929,#51930,#51931,#51932,#51933,#51934,#51935,#51936,#51937,#51938,#51939,
#51940,#51941,#51942,#51943,#51944,#51945,#51946,#51947,#51948,#51949,#51950,
#51951,#51952,#51953,#51954,#51955,#51956,#51957,#51958,#51959,#51960,#51961,
#51962,#51963,#51964,#51965,#51966,#51967,#51968,#51969,#51970,#51971,#51972,
#51973,#51974,#51975,#51976,#51977,#51978,#51979,#51980,#51981,#51982,#51983),
(#51984,#51985,#51986,#51987,#51988,#51989,#51990,#51991,#51992,#51993,
#51994,#51995,#51996,#51997,#51998,#51999,#52000,#52001,#52002,#52003,#52004,
#52005,#52006,#52007,#52008,#52009,#52010,#52011,#52012,#52013,#52014,#52015,
#52016,#52017,#52018,#52019,#52020,#52021,#52022,#52023,#52024,#52025,#52026,
#52027,#52028,#52029,#52030,#52031,#52032,#52033,#52034,#52035,#52036,#52037,
#52038,#52039,#52040,#52041,#52042,#52043,#52044,#52045,#52046,#52047,#52048,
#52049,#52050,#52051,#52052,#52053,#52054,#52055,#52056,#52057,#52058,#52059,
#52060,#52061,#52062,#52063,#52064,#52065,#52066,#52067,#52068,#52069,#52070,
#52071,#52072,#52073,#52074,#52075,#52076,#52077,#52078,#52079,#52080,#52081,
#52082,#52083,#52084,#52085,#52086,#52087,#52088,#52089,#52090,#52091,#52092,
#52093,#52094,#52095,#52096,#52097,#52098),(#52099,#52100,#52101,#52102,
#52103,#52104,#52105,#52106,#52107,#52108,#52109,#52110,#52111,#52112,#52113,
#52114,#52115,#52116,#52117,#52118,#52119,#52120,#52121,#52122,#52123,#52124,
#52125,#52126,#52127,#52128,#52129,#52130,#52131,#52132,#52133,#52134,#52135,
#52136,#52137,#52138,#52139,#52140,#52141,#52142,#52143,#52144,#52145,#52146,
#52147,#52148,#52149,#52150,#52151,#52152,#52153,#52154,#52155,#52156,#52157,
#52158,#52159,#52160,#52161,#52162,#52163,#52164,#52165,#52166,#52167,#52168,
#52169,#52170,#52171,#52172,#52173,#52174,#52175,#52176,#52177,#52178,#52179,
#52180,#52181,#52182,#52183,#52184,#52185,#52186,#52187,#52188,#52189,#52190,
#52191,#52192,#52193,#52194,#52195,#52196,#52197,#52198,#52199,#52200,#52201,
#52202,#52203,#52204,#52205,#52206,#52207,#52208,#52209,#52210,#52211,#52212,
#52213),(#52214,#52215,#52216,#52217,#52218,#52219,#52220,#52221,#52222,
#52223,#52224,#52225,#52226,#52227,#52228,#52229,#52230,#52231,#52232,#52233,
#52234,#52235,#52236,#52237,#52238,#52239,#52240,#52241,#52242,#52243,#52244,
#52245,#52246,#52247,#52248,#52249,#52250,#52251,#52252,#52253,#52254,#52255,
#52256,#52257,#52258,#52259,#52260,#52261,#52262,#52263,#52264,#52265,#52266,
#52267,#52268,#52269,#52270,#52271,#52272,#52273,#52274,#52275,#52276,#52277,
#52278,#52279,#52280,#52281,#52282,#52283,#52284,#52285,#52286,#52287,#52288,
#52289,#52290,#52291,#52292,#52293,#52294,#52295,#52296,#52297,#52298,#52299,
#52300,#52301,#52302,#52303,#52304,#52305,#52306,#52307,#52308,#52309,#52310,
#52311,#52312,#52313,#52314,#52315,#52316,#52317,#52318,#52319,#52320,#52321,
#52322,#52323,#52324,#52325,#52326,#52327,#52328)),.UNSPECIFIED.,.F.,.F.,
 .F.,(4,4),(4,1,1,1,1,1,1,1,1,1,1,1,1,1,1,1,1,1,1,1,1,1,1,1,1,1,1,1,1,1,
1,1,1,1,1,1,1,1,1,1,1,1,1,1,1,1,1,1,1,1,1,1,1,1,1,1,1,1,1,1,1,1,1,1,1,1,
1,1,1,1,1,1,1,1,1,1,1,1,1,1,1,1,1,1,1,1,1,1,1,1,1,1,1,1,1,1,1,1,1,1,1,1,
1,1,1,1,1,1,1,1,1,1,4),(0.,0.173020531651036),(15.1888611523549,15.6834340444711,
16.1780069365874,16.6725798287036,17.1671527208199,17.6617256129361,18.1562985050523,
18.6508713971686,19.1454442892848,19.6400171814011,20.1345900735173,20.6291629656336,
21.1237358577498,21.6183087498661,22.1128816419823,22.6074545340986,23.1020274262148,
23.596600318331,24.0911732104473,24.5857461025635,25.0803189946798,25.574891886796,
26.0694647789123,26.5640376710285,27.0586105631448,27.553183455261,28.0477563473773,
28.5423292394935,29.0369021316097,29.531475023726,30.0260479158422,30.5206208079585,
31.0151937000747,31.509766592191,32.0043394843072,32.4989123764235,32.9934852685397,
33.488058160656,33.9826310527722,34.4772039448884,34.9717768370047,35.4663497291209,
35.9609226212372,36.4554955133534,36.9500684054697,37.4446412975859,37.9392141897022,
38.4337870818184,38.9283599739347,39.4229328660509,39.9175057581671,40.4120786502834,
40.9066515423996,41.4012244345159,41.8957973266321,42.3903702187484,42.8849431108646,
43.3795160029809,43.8740888950971,44.3686617872134,44.8632346793296,45.3578075714458,
45.8523804635621,46.3469533556783,46.8415262477946,47.3360991399108,47.8306720320271,
48.3252449241433,48.8198178162596,49.3143907083758,49.8089636004921,50.3035364926083,
50.7981093847245,51.2926822768408,51.787255168957,52.2818280610733,52.7764009531895,
53.2709738453058,53.765546737422,54.2601196295383,54.7546925216545,55.2492654137708,
55.743838305887,56.2384111980032,56.7329840901195,57.2275569822357,57.722129874352,
58.2167027664682,58.7112756585845,59.2058485507007,59.700421442817,60.1949943349332,
60.6895672270495,61.1841401191657,61.6787130112819,62.1732859033982,62.6678587955144,
63.1624316876307,63.6570045797469,64.1515774718632,64.6461503639794,65.1407232560957,
65.6352961482119,66.1298690403281,66.6244419324444,67.1190148245607,67.6135877166769,
68.1081606087931,68.6027335009094,69.0973063930256,69.5918792851419,70.0864521772581,
70.5810250693744),.UNSPECIFIED.);
#1069=B_SPLINE_CURVE_WITH_KNOTS('',3,(#50266,#50267,#50268,#50269,#50270,
#50271,#50272,#50273,#50274,#50275,#50276,#50277,#50278,#50279,#50280,#50281,
#50282,#50283,#50284,#50285,#50286,#50287,#50288,#50289,#50290),
 .UNSPECIFIED.,.F.,.F.,(4,3,3,3,3,3,3,3,4),(-3.56038179279204,-3.46201024481372,
-2.96743735269747,-2.47286446058123,-1.97829156846498,-1.48371867634874,
-0.989145784232491,-0.494572892116246,0.),.UNSPECIFIED.);
#1070=B_SPLINE_CURVE_WITH_KNOTS('',3,(#50293,#50294,#50295,#50296,#50297,
#50298,#50299,#50300,#50301,#50302,#50303,#50304,#50305,#50306,#50307,#50308,
#50309,#50310,#50311,#50312,#50313,#50314,#50315,#50316,#50317,#50318,#50319,
#50320,#50321,#50322,#50323,#50324,#50325,#50326,#50327,#50328,#50329,#50330,
#50331,#50332),.UNSPECIFIED.,.F.,.F.,(4,3,3,3,3,3,3,3,3,3,3,3,3,4),(0.937891254796418,
0.989145784232494,1.48371867634874,1.97829156846498,2.47286446058123,2.96743735269748,
3.46201024481372,3.95658313692997,4.45115602904621,4.94572892116246,5.44030181327871,
5.93487470539495,6.42944759751119,6.80228742277363),.UNSPECIFIED.);
#1071=B_SPLINE_CURVE_WITH_KNOTS('',3,(#50337,#50338,#50339,#50340,#50341,
#50342,#50343,#50344,#50345,#50346,#50347,#50348,#50349,#50350,#50351,#50352,
#50353,#50354,#50355,#50356,#50357,#50358,#50359,#50360,#50361,#50362,#50363,
#50364,#50365,#50366,#50367,#50368,#50369,#50370,#50371,#50372,#50373,#50374,
#50375,#50376),.UNSPECIFIED.,.F.,.F.,(4,3,3,3,3,3,3,3,3,3,3,3,3,4),(-9.8435670999716,
-9.39688495020867,-8.90231205809242,-8.40773916597618,-7.91316627385993,
-7.41859338174369,-6.92402048962744,-6.42944759751119,-5.93487470539495,
-5.4403018132787,-4.94572892116246,-4.45115602904621,-3.95658313692996,
-3.56038179279204),.UNSPECIFIED.);
#1072=B_SPLINE_CURVE_WITH_KNOTS('',3,(#50377,#50378,#50379,#50380,#50381,
#50382,#50383,#50384,#50385,#50386,#50387,#50388,#50389,#50390,#50391,#50392,
#50393,#50394,#50395,#50396,#50397,#50398,#50399,#50400,#50401,#50402,#50403,
#50404,#50405,#50406,#50407,#50408,#50409,#50410,#50411,#50412,#50413,#50414,
#50415,#50416,#50417,#50418,#50419),.UNSPECIFIED.,.F.,.F.,(4,3,3,3,3,3,
3,3,3,3,3,3,3,3,4),(6.80228742277363,6.92402048962744,7.41859338174369,
7.91316627385993,8.40773916597617,8.90231205809242,9.39688495020867,9.89145784232491,
10.3860307344412,10.8806036265574,11.3751765186736,11.8697494107899,12.3643223029061,
12.8588951950224,13.0854727299532),.UNSPECIFIED.);
#1073=B_SPLINE_CURVE_WITH_KNOTS('',3,(#50424,#50425,#50426,#50427,#50428,
#50429,#50430,#50431,#50432,#50433,#50434,#50435,#50436,#50437,#50438,#50439,
#50440,#50441,#50442,#50443,#50444,#50445,#50446,#50447,#50448,#50449,#50450,
#50451,#50452,#50453,#50454,#50455,#50456,#50457,#50458,#50459,#50460,#50461,
#50462,#50463,#50464,#50465,#50466),.UNSPECIFIED.,.F.,.F.,(4,3,3,3,3,3,
3,3,3,3,3,3,3,3,4),(-16.1267524071512,-15.8263325477199,-15.3317596556036,
-14.8371867634874,-14.3426138713711,-13.8480409792549,-13.3534680871386,
-12.8588951950224,-12.3643223029061,-11.8697494107899,-11.3751765186736,
-10.8806036265574,-10.3860307344412,-9.89145784232491,-9.8435670999716),
 .UNSPECIFIED.);
#1074=B_SPLINE_CURVE_WITH_KNOTS('',3,(#50467,#50468,#50469,#50470,#50471,
#50472,#50473,#50474,#50475,#50476,#50477,#50478,#50479,#50480,#50481,#50482,
#50483,#50484,#50485,#50486,#50487,#50488,#50489,#50490,#50491,#50492,#50493,
#50494,#50495,#50496,#50497,#50498,#50499,#50500,#50501,#50502,#50503,#50504,
#50505,#50506,#50507,#50508,#50509),.UNSPECIFIED.,.F.,.F.,(4,3,3,3,3,3,
3,3,3,3,3,3,3,3,4),(13.0854727299532,13.3534680871386,13.8480409792549,
14.3426138713711,14.8371867634874,15.3317596556036,15.8263325477199,16.3209054398361,
16.8154783319523,17.3100512240686,17.8046241161848,18.2991970083011,18.7937699004173,
19.2883427925336,19.3686580371328),.UNSPECIFIED.);
#1075=B_SPLINE_CURVE_WITH_KNOTS('',3,(#50514,#50515,#50516,#50517,#50518,
#50519,#50520,#50521,#50522,#50523,#50524,#50525,#50526,#50527,#50528,#50529,
#50530,#50531,#50532,#50533,#50534,#50535,#50536,#50537,#50538,#50539,#50540,
#50541,#50542,#50543,#50544,#50545,#50546,#50547,#50548,#50549,#50550,#50551,
#50552,#50553,#50554,#50555,#50556),.UNSPECIFIED.,.F.,.F.,(4,3,3,3,3,3,
3,3,3,3,3,3,3,3,4),(-22.4099377143308,-22.2557801452311,-21.7612072531148,
-21.2666343609986,-20.7720614688823,-20.2774885767661,-19.7829156846498,
-19.2883427925336,-18.7937699004173,-18.2991970083011,-17.8046241161848,
-17.3100512240686,-16.8154783319523,-16.3209054398361,-16.1267524071512),
 .UNSPECIFIED.);
#1076=B_SPLINE_CURVE_WITH_KNOTS('',3,(#50557,#50558,#50559,#50560,#50561,
#50562,#50563,#50564,#50565,#50566,#50567,#50568,#50569,#50570,#50571,#50572,
#50573,#50574,#50575,#50576,#50577,#50578,#50579,#50580,#50581,#50582,#50583,
#50584,#50585,#50586,#50587,#50588,#50589,#50590,#50591,#50592,#50593,#50594,
#50595,#50596),.UNSPECIFIED.,.F.,.F.,(4,3,3,3,3,3,3,3,3,3,3,3,3,4),(19.3686580371328,
19.7829156846498,20.2774885767661,20.7720614688823,21.2666343609986,21.7612072531148,
22.255780145231,22.7503530373473,23.2449259294635,23.7394988215798,24.234071713696,
24.7286446058123,25.2232174979285,25.6518433443124),.UNSPECIFIED.);
#1077=B_SPLINE_CURVE_WITH_KNOTS('',3,(#50601,#50602,#50603,#50604,#50605,
#50606,#50607,#50608,#50609,#50610,#50611,#50612,#50613,#50614,#50615,#50616,
#50617,#50618,#50619,#50620,#50621,#50622,#50623,#50624,#50625,#50626,#50627,
#50628,#50629,#50630,#50631,#50632,#50633,#50634,#50635,#50636,#50637,#50638,
#50639,#50640,#50641,#50642,#50643),.UNSPECIFIED.,.F.,.F.,(4,3,3,3,3,3,
3,3,3,3,3,3,3,3,4),(-28.6931230215104,-28.6852277427422,-28.190654850626,
-27.6960819585097,-27.2015090663935,-26.7069361742773,-26.212363282161,
-25.7177903900448,-25.2232174979285,-24.7286446058123,-24.234071713696,
-23.7394988215798,-23.2449259294635,-22.7503530373473,-22.4099377143308),
 .UNSPECIFIED.);
#1078=B_SPLINE_CURVE_WITH_KNOTS('',3,(#50644,#50645,#50646,#50647,#50648,
#50649,#50650,#50651,#50652,#50653,#50654,#50655,#50656,#50657,#50658,#50659,
#50660,#50661,#50662,#50663,#50664,#50665,#50666,#50667,#50668,#50669,#50670,
#50671,#50672,#50673,#50674,#50675,#50676,#50677,#50678,#50679,#50680,#50681,
#50682,#50683,#50684,#50685,#50686),.UNSPECIFIED.,.F.,.F.,(4,3,3,3,3,3,
3,3,3,3,3,3,3,3,4),(25.6518433443124,25.7177903900448,26.212363282161,26.7069361742773,
27.2015090663935,27.6960819585097,28.190654850626,28.6852277427422,29.1798006348585,
29.6743735269747,30.168946419091,30.6635193112072,31.1580922033235,31.6526650954397,
31.935028651492),.UNSPECIFIED.);
#1079=B_SPLINE_CURVE_WITH_KNOTS('',3,(#50691,#50692,#50693,#50694,#50695,
#50696,#50697,#50698,#50699,#50700,#50701,#50702,#50703,#50704,#50705,#50706,
#50707,#50708,#50709,#50710,#50711,#50712,#50713,#50714,#50715,#50716,#50717,
#50718,#50719,#50720,#50721,#50722,#50723,#50724,#50725,#50726,#50727,#50728,
#50729,#50730),.UNSPECIFIED.,.F.,.F.,(4,3,3,3,3,3,3,3,3,3,3,3,3,4),(-34.97630832869,
-34.6201024481372,-34.1255295560209,-33.6309566639047,-33.1363837717884,
-32.6418108796722,-32.147237987556,-31.6526650954397,-31.1580922033235,
-30.6635193112072,-30.168946419091,-29.6743735269747,-29.1798006348585,
-28.6931230215104),.UNSPECIFIED.);
#1080=B_SPLINE_CURVE_WITH_KNOTS('',3,(#50731,#50732,#50733,#50734,#50735,
#50736,#50737,#50738,#50739,#50740,#50741,#50742,#50743,#50744,#50745,#50746,
#50747,#50748,#50749,#50750,#50751,#50752,#50753,#50754,#50755,#50756,#50757,
#50758,#50759,#50760,#50761,#50762,#50763,#50764,#50765,#50766,#50767,#50768,
#50769,#50770,#50771,#50772,#50773),.UNSPECIFIED.,.F.,.F.,(4,3,3,3,3,3,
3,3,3,3,3,3,3,3,4),(31.935028651492,32.147237987556,32.6418108796722,33.1363837717885,
33.6309566639047,34.1255295560209,34.6201024481372,35.1146753402534,35.6092482323697,
36.1038211244859,36.5983940166022,37.0929669087184,37.5875398008347,38.0821126929509,
38.2182139586716),.UNSPECIFIED.);
#1081=B_SPLINE_CURVE_WITH_KNOTS('',3,(#50778,#50779,#50780,#50781,#50782,
#50783,#50784,#50785,#50786,#50787,#50788,#50789,#50790,#50791,#50792,#50793,
#50794,#50795,#50796,#50797,#50798,#50799,#50800,#50801,#50802,#50803,#50804,
#50805,#50806,#50807,#50808,#50809,#50810,#50811,#50812,#50813,#50814,#50815,
#50816,#50817,#50818,#50819,#50820),.UNSPECIFIED.,.F.,.F.,(4,3,3,3,3,3,
3,3,3,3,3,3,3,3,4),(-41.2594936358696,-41.0495500456484,-40.5549771535321,
-40.0604042614159,-39.5658313692996,-39.0712584771834,-38.5766855850671,
-38.0821126929509,-37.5875398008347,-37.0929669087184,-36.5983940166022,
-36.1038211244859,-35.6092482323697,-35.1146753402534,-34.97630832869),
 .UNSPECIFIED.);
#1082=B_SPLINE_CURVE_WITH_KNOTS('',3,(#50821,#50822,#50823,#50824,#50825,
#50826,#50827,#50828,#50829,#50830,#50831,#50832,#50833,#50834,#50835,#50836,
#50837,#50838,#50839,#50840,#50841,#50842,#50843,#50844,#50845,#50846,#50847,
#50848,#50849,#50850,#50851,#50852,#50853,#50854,#50855,#50856,#50857,#50858,
#50859,#50860),.UNSPECIFIED.,.F.,.F.,(4,3,3,3,3,3,3,3,3,3,3,3,3,4),(38.2182139586716,
38.5766855850671,39.0712584771834,39.5658313692996,40.0604042614159,40.5549771535321,
41.0495500456484,41.5441229377646,42.0386958298809,42.5332687219971,43.0278416141134,
43.5224145062296,44.0169873983459,44.5013992658512),.UNSPECIFIED.);
#1083=B_SPLINE_CURVE_WITH_KNOTS('',3,(#50865,#50866,#50867,#50868,#50869,
#50870,#50871,#50872,#50873,#50874,#50875,#50876,#50877,#50878,#50879,#50880,
#50881,#50882,#50883,#50884,#50885,#50886,#50887,#50888,#50889,#50890,#50891,
#50892,#50893,#50894,#50895,#50896,#50897,#50898,#50899,#50900,#50901,#50902,
#50903,#50904,#50905,#50906,#50907),.UNSPECIFIED.,.F.,.F.,(4,3,3,3,3,3,
3,3,3,3,3,3,3,3,4),(-47.5426789430491,-47.4789976431596,-46.9844247510433,
-46.4898518589271,-45.9952789668108,-45.5007060746946,-45.0061331825783,
-44.5115602904621,-44.0169873983458,-43.5224145062296,-43.0278416141134,
-42.5332687219971,-42.0386958298809,-41.5441229377646,-41.2594936358696),
 .UNSPECIFIED.);
#1084=B_SPLINE_CURVE_WITH_KNOTS('',3,(#50908,#50909,#50910,#50911,#50912,
#50913,#50914,#50915,#50916,#50917,#50918,#50919,#50920,#50921,#50922,#50923,
#50924,#50925,#50926,#50927,#50928,#50929,#50930,#50931,#50932,#50933,#50934,
#50935,#50936,#50937,#50938,#50939,#50940,#50941,#50942,#50943,#50944,#50945,
#50946,#50947,#50948,#50949,#50950),.UNSPECIFIED.,.F.,.F.,(4,3,3,3,3,3,
3,3,3,3,3,3,3,3,4),(44.5013992658512,44.5115602904621,45.0061331825783,
45.5007060746946,45.9952789668108,46.4898518589271,46.9844247510433,47.4789976431596,
47.9735705352758,48.4681434273921,48.9627163195083,49.4572892116245,49.9518621037408,
50.446434995857,50.7845845730308),.UNSPECIFIED.);
#1085=B_SPLINE_CURVE_WITH_KNOTS('',3,(#50957,#50958,#50959,#50960,#50961,
#50962,#50963,#50964,#50965,#50966),.UNSPECIFIED.,.F.,.F.,(4,3,3,4),(-54.4542726622231,
-54.403018132787,-53.9084452406708,-53.8258642502287),.UNSPECIFIED.);
#1086=B_SPLINE_CURVE_WITH_KNOTS('',3,(#50972,#50973,#50974,#50975,#50976,
#50977,#50978),.UNSPECIFIED.,.F.,.F.,(4,1,1,1,4),(65.9734457253856,66.0560267158277,
66.5505996079439,67.0451725000601,67.5397453921764),.UNSPECIFIED.);
#1087=B_SPLINE_CURVE_WITH_KNOTS('',3,(#50981,#50982,#50983,#50984,#50985,
#50986,#50987,#50988,#50989,#50990,#50991,#50992),.UNSPECIFIED.,.F.,.F.,
(4,1,1,1,1,1,1,1,1,4),(65.9734457253856,66.1298690403281,66.6244419324444,
67.1190148245607,67.6135877166769,68.1081606087931,68.6027335009094,69.0973063930256,
69.5918792851419,69.643133814578),.UNSPECIFIED.);
#1088=B_SPLINE_CURVE_WITH_KNOTS('',3,(#50997,#50998,#50999,#51000,#51001,
#51002,#51003,#51004,#51005,#51006,#51007,#51008,#51009,#51010,#51011,#51012),
 .UNSPECIFIED.,.F.,.F.,(4,1,1,1,1,1,1,1,1,1,1,1,1,4),(59.6902604182061,
60.1211520104327,60.615724902549,61.1102977946652,61.6048706867815,62.0994435788977,
62.5940164710139,63.0885893631302,63.5831622552464,64.0777351473627,64.5723080394789,
65.0668809315952,65.5614538237114,65.9734457253856),.UNSPECIFIED.);
#1089=B_SPLINE_CURVE_WITH_KNOTS('',3,(#51013,#51014,#51015,#51016,#51017,
#51018,#51019,#51020,#51021,#51022,#51023,#51024,#51025,#51026,#51027,#51028,
#51029),.UNSPECIFIED.,.F.,.F.,(4,1,1,1,1,1,1,1,1,1,1,1,1,1,4),(59.6902604182061,
59.700421442817,60.1949943349332,60.6895672270495,61.1841401191657,61.6787130112819,
62.1732859033982,62.6678587955144,63.1624316876307,63.6570045797469,64.1515774718632,
64.6461503639794,65.1407232560957,65.6352961482119,65.9734457253856),
 .UNSPECIFIED.);
#1090=B_SPLINE_CURVE_WITH_KNOTS('',3,(#51034,#51035,#51036,#51037,#51038,
#51039,#51040,#51041,#51042,#51043,#51044,#51045,#51046,#51047,#51048,#51049,
#51050),.UNSPECIFIED.,.F.,.F.,(4,1,1,1,1,1,1,1,1,1,1,1,1,1,4),(53.4070751110264,
53.6917044129215,54.1862773050378,54.680850197154,55.1754230892703,55.6699959813865,
56.1645688735028,56.659141765619,57.1537146577353,57.6482875498515,58.1428604419677,
58.637433334084,59.1320062262002,59.6265791183165,59.6902604182061),
 .UNSPECIFIED.);
#1091=B_SPLINE_CURVE_WITH_KNOTS('',3,(#51051,#51052,#51053,#51054,#51055,
#51056,#51057,#51058,#51059,#51060,#51061,#51062,#51063,#51064,#51065,#51066),
 .UNSPECIFIED.,.F.,.F.,(4,1,1,1,1,1,1,1,1,1,1,1,1,4),(53.4070751110264,
53.765546737422,54.2601196295383,54.7546925216545,55.2492654137708,55.743838305887,
56.2384111980032,56.7329840901195,57.2275569822357,57.722129874352,58.2167027664682,
58.7112756585845,59.2058485507007,59.6902604182061),.UNSPECIFIED.);
#1092=B_SPLINE_CURVE_WITH_KNOTS('',3,(#51071,#51072,#51073,#51074,#51075,
#51076,#51077,#51078,#51079,#51080,#51081,#51082,#51083,#51084,#51085,#51086,
#51087),.UNSPECIFIED.,.F.,.F.,(4,1,1,1,1,1,1,1,1,1,1,1,1,1,4),(47.1238898038469,
47.2622568154103,47.7568297075266,48.2514025996428,48.7459754917591,49.2405483838753,
49.7351212759916,50.2296941681078,50.7242670602241,51.2188399523403,51.7134128444565,
52.2079857365728,52.702558628689,53.1971315208053,53.4070751110264),
 .UNSPECIFIED.);
#1093=B_SPLINE_CURVE_WITH_KNOTS('',3,(#51088,#51089,#51090,#51091,#51092,
#51093,#51094,#51095,#51096,#51097,#51098,#51099,#51100,#51101,#51102,#51103,
#51104),.UNSPECIFIED.,.F.,.F.,(4,1,1,1,1,1,1,1,1,1,1,1,1,1,4),(47.1238898038469,
47.3360991399108,47.8306720320271,48.3252449241433,48.8198178162596,49.3143907083758,
49.8089636004921,50.3035364926083,50.7981093847245,51.2926822768408,51.787255168957,
52.2818280610733,52.7764009531895,53.2709738453058,53.4070751110264),
 .UNSPECIFIED.);
#1094=B_SPLINE_CURVE_WITH_KNOTS('',3,(#51109,#51110,#51111,#51112,#51113,
#51114,#51115,#51116,#51117,#51118,#51119,#51120,#51121,#51122,#51123,#51124),
 .UNSPECIFIED.,.F.,.F.,(4,1,1,1,1,1,1,1,1,1,1,1,1,4),(40.8407044966673,
41.3273821100154,41.8219550021316,42.3165278942479,42.8111007863641,43.3056736784804,
43.8002465705966,44.2948194627129,44.7893923548291,45.2839652469454,45.7785381390616,
46.2731110311778,46.7676839232941,47.1238898038469),.UNSPECIFIED.);
#1095=B_SPLINE_CURVE_WITH_KNOTS('',3,(#51125,#51126,#51127,#51128,#51129,
#51130,#51131,#51132,#51133,#51134,#51135,#51136,#51137,#51138,#51139,#51140,
#51141),.UNSPECIFIED.,.F.,.F.,(4,1,1,1,1,1,1,1,1,1,1,1,1,1,4),(40.8407044966673,
40.9066515423996,41.4012244345159,41.8957973266321,42.3903702187484,42.8849431108646,
43.3795160029809,43.8740888950971,44.3686617872134,44.8632346793296,45.3578075714458,
45.8523804635621,46.3469533556783,46.8415262477946,47.1238898038469),
 .UNSPECIFIED.);
#1096=B_SPLINE_CURVE_WITH_KNOTS('',3,(#51146,#51147,#51148,#51149,#51150,
#51151,#51152,#51153,#51154,#51155,#51156,#51157,#51158,#51159,#51160,#51161,
#51162),.UNSPECIFIED.,.F.,.F.,(4,1,1,1,1,1,1,1,1,1,1,1,1,1,4),(34.5575191894877,
34.8979345125042,35.3925074046204,35.8870802967367,36.3816531888529,36.8762260809692,
37.3707989730854,37.8653718652017,38.3599447573179,38.8545176494342,39.3490905415504,
39.8436634336667,40.3382363257829,40.8328092178991,40.8407044966673),
 .UNSPECIFIED.);
#1097=B_SPLINE_CURVE_WITH_KNOTS('',3,(#51163,#51164,#51165,#51166,#51167,
#51168,#51169,#51170,#51171,#51172,#51173,#51174,#51175,#51176,#51177,#51178),
 .UNSPECIFIED.,.F.,.F.,(4,1,1,1,1,1,1,1,1,1,1,1,1,4),(34.5575191894877,
34.9717768370047,35.4663497291209,35.9609226212372,36.4554955133534,36.9500684054697,
37.4446412975859,37.9392141897022,38.4337870818184,38.9283599739347,39.4229328660509,
39.9175057581671,40.4120786502834,40.8407044966673),.UNSPECIFIED.);
#1098=B_SPLINE_CURVE_WITH_KNOTS('',3,(#51183,#51184,#51185,#51186,#51187,
#51188,#51189,#51190,#51191,#51192,#51193,#51194,#51195,#51196,#51197,#51198,
#51199),.UNSPECIFIED.,.F.,.F.,(4,1,1,1,1,1,1,1,1,1,1,1,1,1,4),(28.2743338823081,
28.468486914993,28.9630598071093,29.4576326992255,29.9522055913417,30.446778483458,
30.9413513755742,31.4359242676905,31.9304971598067,32.425070051923,32.9196429440392,
33.4142158361555,33.9087887282717,34.403361620388,34.5575191894877),
 .UNSPECIFIED.);
#1099=B_SPLINE_CURVE_WITH_KNOTS('',3,(#51200,#51201,#51202,#51203,#51204,
#51205,#51206,#51207,#51208,#51209,#51210,#51211,#51212,#51213,#51214,#51215,
#51216),.UNSPECIFIED.,.F.,.F.,(4,1,1,1,1,1,1,1,1,1,1,1,1,1,4),(28.2743338823081,
28.5423292394935,29.0369021316097,29.531475023726,30.0260479158422,30.5206208079585,
31.0151937000747,31.509766592191,32.0043394843072,32.4989123764235,32.9934852685397,
33.488058160656,33.9826310527722,34.4772039448884,34.5575191894877),
 .UNSPECIFIED.);
#1100=B_SPLINE_CURVE_WITH_KNOTS('',3,(#51221,#51222,#51223,#51224,#51225,
#51226,#51227,#51228,#51229,#51230,#51231,#51232,#51233,#51234,#51235,#51236,
#51237),.UNSPECIFIED.,.F.,.F.,(4,1,1,1,1,1,1,1,1,1,1,1,1,1,4),(21.9911485751285,
22.0390393174818,22.5336122095981,23.0281851017143,23.5227579938306,24.0173308859468,
24.511903778063,25.0064766701793,25.5010495622955,25.9956224544118,26.490195346528,
26.9847682386443,27.4793411307605,27.9739140228768,28.2743338823081),
 .UNSPECIFIED.);
#1101=B_SPLINE_CURVE_WITH_KNOTS('',3,(#51238,#51239,#51240,#51241,#51242,
#51243,#51244,#51245,#51246,#51247,#51248,#51249,#51250,#51251,#51252,#51253,
#51254),.UNSPECIFIED.,.F.,.F.,(4,1,1,1,1,1,1,1,1,1,1,1,1,1,4),(21.9911485751285,
22.1128816419823,22.6074545340986,23.1020274262148,23.596600318331,24.0911732104473,
24.5857461025635,25.0803189946798,25.574891886796,26.0694647789123,26.5640376710285,
27.0586105631448,27.553183455261,28.0477563473773,28.2743338823081),
 .UNSPECIFIED.);
#1102=B_SPLINE_CURVE_WITH_KNOTS('',3,(#51260,#51261,#51262,#51263,#51264),
 .UNSPECIFIED.,.F.,.F.,(4,1,4),(15.1888611523549,15.6834340444711,15.7079632679489),
 .UNSPECIFIED.);
#1103=B_SPLINE_CURVE_WITH_KNOTS('',3,(#51267,#51268,#51269,#51270,#51271,
#51272,#51273,#51274,#51275,#51276),.UNSPECIFIED.,.F.,.F.,(4,1,1,1,1,1,
1,4),(13.0854727299533,13.1367272593894,13.6313001515056,14.1258730436219,
14.6204459357381,15.1150188278544,15.6095917199706,15.7079632679489),
 .UNSPECIFIED.);
#1104=B_SPLINE_CURVE_WITH_KNOTS('',3,(#51278,#51279,#51280,#51281,#51282,
#51283,#51284,#51285,#51286,#51287,#51288,#51289,#51290,#51291,#51292,#51293),
 .UNSPECIFIED.,.F.,.F.,(4,1,1,1,1,1,1,1,1,1,1,1,1,4),(15.7079632679489,
16.1041646120869,16.5987375042031,17.0933103963194,17.5878832884356,18.0824561805519,
18.5770290726681,19.0716019647843,19.5661748569006,20.0607477490168,20.5553206411331,
21.0498935332493,21.5444664253656,21.9911485751285),.UNSPECIFIED.);
#1105=B_SPLINE_CURVE_WITH_KNOTS('',3,(#51294,#51295,#51296,#51297,#51298,
#51299,#51300,#51301,#51302,#51303,#51304,#51305,#51306,#51307,#51308,#51309),
 .UNSPECIFIED.,.F.,.F.,(4,1,1,1,1,1,1,1,1,1,1,1,1,4),(15.7079632679489,
16.1780069365874,16.6725798287036,17.1671527208199,17.6617256129361,18.1562985050523,
18.6508713971686,19.1454442892848,19.6400171814011,20.1345900735173,20.6291629656336,
21.1237358577498,21.6183087498661,21.9911485751285),.UNSPECIFIED.);
#1106=B_SPLINE_CURVE_WITH_KNOTS('',3,(#51770,#51771,#51772,#51773,#51774,
#51775,#51776,#51777,#51778,#51779,#51780,#51781,#51782,#51783,#51784,#51785,
#51786,#51787,#51788,#51789,#51790,#51791,#51792,#51793,#51794,#51795,#51796,
#51797,#51798,#51799,#51800),.UNSPECIFIED.,.F.,.F.,(4,3,3,3,3,3,3,3,3,3,
4),(0.,0.0822466706468383,0.162608105240606,0.216579893838171,0.23924274204394,
0.301838371937517,0.36076250940623,0.388067588559334,0.409537377502954,
0.476290104322315,0.53753492181237),.UNSPECIFIED.);
#1107=B_SPLINE_CURVE_WITH_KNOTS('',3,(#51801,#51802,#51803,#51804,#51805,
#51806,#51807,#51808,#51809,#51810,#51811,#51812,#51813,#51814,#51815,#51816,
#51817,#51818,#51819,#51820,#51821,#51822,#51823,#51824,#51825,#51826,#51827,
#51828),.UNSPECIFIED.,.F.,.F.,(4,3,3,3,3,3,3,3,3,4),(0.,0.0665230127441691,
0.13429495842692,0.176258819244205,0.195926107024299,0.263526952009386,
0.33682854572103,0.365338415901403,0.449700157257057,0.534061898612711),
 .UNSPECIFIED.);
#1108=B_SPLINE_CURVE_WITH_KNOTS('',3,(#51829,#51830,#51831,#51832,#51833,
#51834,#51835,#51836,#51837,#51838,#51839,#51840,#51841,#51842,#51843,#51844,
#51845,#51846,#51847,#51848,#51849,#51850,#51851,#51852,#51853,#51854,#51855,
#51856,#51857,#51858,#51859,#51860,#51861,#51862,#51863,#51864,#51865,#51866,
#51867,#51868),.UNSPECIFIED.,.F.,.F.,(4,3,3,3,3,3,3,3,3,3,3,3,3,4),(-53.8258642502287,
-53.4138723485545,-52.9192994564383,-52.424726564322,-51.9301536722058,
-51.4355807800895,-50.9410078879733,-50.446434995857,-49.9518621037408,
-49.4572892116245,-48.9627163195083,-48.4681434273921,-47.9735705352758,
-47.5426789430491),.UNSPECIFIED.);
#1109=B_SPLINE_CURVE_WITH_KNOTS('',3,(#52330,#52331,#52332,#52333,#52334,
#52335,#52336,#52337,#52338,#52339,#52340,#52341,#52342,#52343,#52344,#52345,
#52346,#52347,#52348,#52349,#52350,#52351,#52352,#52353,#52354,#52355,#52356,
#52357),.UNSPECIFIED.,.F.,.F.,(4,3,3,3,3,3,3,3,3,4),(0.,0.0665230199567328,
0.134294967830964,0.176258831509978,0.195926124443112,0.263526952009376,
0.336828549458816,0.365338416771381,0.449700157692121,0.534061898612861),
 .UNSPECIFIED.);
#1110=B_SPLINE_CURVE_WITH_KNOTS('',3,(#52358,#52359,#52360,#52361,#52362,
#52363,#52364,#52365,#52366,#52367,#52368,#52369,#52370,#52371,#52372,#52373,
#52374,#52375,#52376,#52377,#52378,#52379,#52380,#52381,#52382,#52383,#52384,
#52385,#52386,#52387,#52388),.UNSPECIFIED.,.F.,.F.,(4,3,3,3,3,3,3,3,3,3,
4),(50.7845845730308,50.9410078879733,51.4355807800895,51.9301536722058,
52.424726564322,52.9192994564383,53.4138723485545,53.9084452406708,54.403018132787,
54.8975910249033,55.3921639170195),.UNSPECIFIED.);
#1111=B_SPLINE_CURVE_WITH_KNOTS('',3,(#52389,#52390,#52391,#52392,#52393,
#52394,#52395,#52396,#52397,#52398,#52399,#52400,#52401,#52402,#52403,#52404,
#52405,#52406,#52407,#52408,#52409,#52410,#52411,#52412,#52413,#52414,#52415,
#52416,#52417,#52418,#52419),.UNSPECIFIED.,.F.,.F.,(4,3,3,3,3,3,3,3,3,3,
4),(0.,0.0822466663612967,0.162608100396307,0.216579890867136,0.239242742625966,
0.301838371937549,0.360762509406336,0.388067584071394,0.409537375230468,
0.476290092032249,0.537534921812695),.UNSPECIFIED.);
#1574=SHAPE_REPRESENTATION_RELATIONSHIP('SRR','None',#63433,#1657);
#1657=ADVANCED_BREP_SHAPE_REPRESENTATION('',(#1877),#62970);
#1770=STYLED_ITEM('',(#63919),#1877);
#1877=MANIFOLD_SOLID_BREP('Body1',#23070);
#2261=FACE_BOUND('',#5610,.T.);
#2262=FACE_BOUND('',#5611,.T.);
#2263=FACE_BOUND('',#5612,.T.);
#2264=FACE_BOUND('',#5613,.T.);
#2265=FACE_BOUND('',#5619,.T.);
#2266=FACE_BOUND('',#5620,.T.);
#2267=FACE_BOUND('',#5621,.T.);
#2268=FACE_BOUND('',#5622,.T.);
#2269=FACE_BOUND('',#5627,.T.);
#2783=PLANE('',#26033);
#2784=PLANE('',#26045);
#2785=PLANE('',#26046);
#2786=PLANE('',#26053);
#3900=FACE_OUTER_BOUND('',#5588,.T.);
#3901=FACE_OUTER_BOUND('',#5589,.T.);
#3902=FACE_OUTER_BOUND('',#5590,.T.);
#3903=FACE_OUTER_BOUND('',#5591,.T.);
#3904=FACE_OUTER_BOUND('',#5592,.T.);
#3905=FACE_OUTER_BOUND('',#5593,.T.);
#3906=FACE_OUTER_BOUND('',#5594,.T.);
#3907=FACE_OUTER_BOUND('',#5595,.T.);
#3908=FACE_OUTER_BOUND('',#5596,.T.);
#3909=FACE_OUTER_BOUND('',#5597,.T.);
#3910=FACE_OUTER_BOUND('',#5598,.T.);
#3911=FACE_OUTER_BOUND('',#5599,.T.);
#3912=FACE_OUTER_BOUND('',#5600,.T.);
#3913=FACE_OUTER_BOUND('',#5601,.T.);
#3914=FACE_OUTER_BOUND('',#5602,.T.);
#3915=FACE_OUTER_BOUND('',#5603,.T.);
#3916=FACE_OUTER_BOUND('',#5604,.T.);
#3917=FACE_OUTER_BOUND('',#5605,.T.);
#3918=FACE_OUTER_BOUND('',#5606,.T.);
#3919=FACE_OUTER_BOUND('',#5607,.T.);
#3920=FACE_OUTER_BOUND('',#5608,.T.);
#3921=FACE_OUTER_BOUND('',#5609,.T.);
#3922=FACE_OUTER_BOUND('',#5614,.T.);
#3923=FACE_OUTER_BOUND('',#5615,.T.);
#3924=FACE_OUTER_BOUND('',#5616,.T.);
#3925=FACE_OUTER_BOUND('',#5617,.T.);
#3926=FACE_OUTER_BOUND('',#5618,.T.);
#3927=FACE_OUTER_BOUND('',#5623,.T.);
#3928=FACE_OUTER_BOUND('',#5624,.T.);
#3929=FACE_OUTER_BOUND('',#5625,.T.);
#3930=FACE_OUTER_BOUND('',#5626,.T.);
#5588=EDGE_LOOP('',(#19612,#19613,#19614,#19615));
#5589=EDGE_LOOP('',(#19616,#19617,#19618,#19619));
#5590=EDGE_LOOP('',(#19620,#19621,#19622,#19623));
#5591=EDGE_LOOP('',(#19624,#19625,#19626,#19627));
#5592=EDGE_LOOP('',(#19628,#19629,#19630,#19631));
#5593=EDGE_LOOP('',(#19632,#19633,#19634,#19635));
#5594=EDGE_LOOP('',(#19636,#19637,#19638,#19639));
#5595=EDGE_LOOP('',(#19640,#19641,#19642,#19643));
#5596=EDGE_LOOP('',(#19644,#19645,#19646));
#5597=EDGE_LOOP('',(#19647,#19648,#19649,#19650));
#5598=EDGE_LOOP('',(#19651,#19652,#19653,#19654));
#5599=EDGE_LOOP('',(#19655,#19656,#19657,#19658));
#5600=EDGE_LOOP('',(#19659,#19660,#19661,#19662));
#5601=EDGE_LOOP('',(#19663,#19664,#19665,#19666));
#5602=EDGE_LOOP('',(#19667,#19668,#19669,#19670));
#5603=EDGE_LOOP('',(#19671,#19672,#19673,#19674));
#5604=EDGE_LOOP('',(#19675,#19676,#19677,#19678));
#5605=EDGE_LOOP('',(#19679,#19680,#19681,#19682));
#5606=EDGE_LOOP('',(#19683,#19684,#19685,#19686));
#5607=EDGE_LOOP('',(#19687,#19688,#19689,#19690,#19691,#19692,#19693,#19694,
#19695,#19696,#19697,#19698,#19699,#19700,#19701,#19702,#19703,#19704,#19705,
#19706,#19707,#19708));
#5608=EDGE_LOOP('',(#19709,#19710,#19711,#19712,#19713,#19714,#19715,#19716,
#19717,#19718,#19719,#19720,#19721,#19722,#19723,#19724,#19725,#19726,#19727,
#19728,#19729));
#5609=EDGE_LOOP('',(#19730,#19731));
#5610=EDGE_LOOP('',(#19732,#19733,#19734,#19735,#19736));
#5611=EDGE_LOOP('',(#19737));
#5612=EDGE_LOOP('',(#19738));
#5613=EDGE_LOOP('',(#19739));
#5614=EDGE_LOOP('',(#19740,#19741,#19742,#19743));
#5615=EDGE_LOOP('',(#19744,#19745,#19746,#19747));
#5616=EDGE_LOOP('',(#19748,#19749,#19750,#19751));
#5617=EDGE_LOOP('',(#19752,#19753,#19754,#19755));
#5618=EDGE_LOOP('',(#19756,#19757));
#5619=EDGE_LOOP('',(#19758));
#5620=EDGE_LOOP('',(#19759));
#5621=EDGE_LOOP('',(#19760));
#5622=EDGE_LOOP('',(#19761));
#5623=EDGE_LOOP('',(#19762,#19763,#19764,#19765));
#5624=EDGE_LOOP('',(#19766,#19767,#19768,#19769,#19770));
#5625=EDGE_LOOP('',(#19771,#19772,#19773,#19774));
#5626=EDGE_LOOP('',(#19775));
#5627=EDGE_LOOP('',(#19776,#19777,#19778,#19779));
#7079=LINE('',#50264,#8566);
#7080=LINE('',#50336,#8567);
#7081=LINE('',#50423,#8568);
#7082=LINE('',#50513,#8569);
#7083=LINE('',#50600,#8570);
#7084=LINE('',#50690,#8571);
#7085=LINE('',#50777,#8572);
#7086=LINE('',#50864,#8573);
#7087=LINE('',#50954,#8574);
#7088=LINE('',#50970,#8575);
#7089=LINE('',#50996,#8576);
#7090=LINE('',#51033,#8577);
#7091=LINE('',#51070,#8578);
#7092=LINE('',#51108,#8579);
#7093=LINE('',#51145,#8580);
#7094=LINE('',#51182,#8581);
#7095=LINE('',#51220,#8582);
#7096=LINE('',#51258,#8583);
#7097=LINE('',#52423,#8584);
#7098=LINE('',#52435,#8585);
#7099=LINE('',#52439,#8586);
#7100=LINE('',#52443,#8587);
#7101=LINE('',#52447,#8588);
#7102=LINE('',#52448,#8589);
#7103=LINE('',#52449,#8590);
#7104=LINE('',#52458,#8591);
#8566=VECTOR('',#31656,0.45);
#8567=VECTOR('',#31661,0.45);
#8568=VECTOR('',#31664,0.45);
#8569=VECTOR('',#31667,0.45);
#8570=VECTOR('',#31670,0.45);
#8571=VECTOR('',#31673,0.45);
#8572=VECTOR('',#31676,0.45);
#8573=VECTOR('',#31679,0.45);
#8574=VECTOR('',#31682,0.45);
#8575=VECTOR('',#31687,0.625);
#8576=VECTOR('',#31692,0.625);
#8577=VECTOR('',#31695,0.625);
#8578=VECTOR('',#31698,0.625);
#8579=VECTOR('',#31701,0.625);
#8580=VECTOR('',#31704,0.625);
#8581=VECTOR('',#31707,0.625);
#8582=VECTOR('',#31710,0.625);
#8583=VECTOR('',#31713,0.625);
#8584=VECTOR('',#31720,1.);
#8585=VECTOR('',#31735,0.225);
#8586=VECTOR('',#31740,0.225);
#8587=VECTOR('',#31745,0.225);
#8588=VECTOR('',#31748,1.);
#8589=VECTOR('',#31749,1.);
#8590=VECTOR('',#31750,1.);
#8591=VECTOR('',#31763,1.1);
#9685=CIRCLE('',#26011,0.457875);
#9686=CIRCLE('',#26020,0.457875);
#9687=CIRCLE('',#26022,0.625);
#9688=CIRCLE('',#26031,0.625);
#9689=CIRCLE('',#26034,1.9);
#9690=CIRCLE('',#26035,0.457875);
#9691=CIRCLE('',#26036,0.225);
#9692=CIRCLE('',#26037,0.225);
#9693=CIRCLE('',#26038,0.225);
#9694=CIRCLE('',#26040,0.225);
#9695=CIRCLE('',#26042,0.225);
#9696=CIRCLE('',#26044,0.225);
#9697=CIRCLE('',#26047,1.9);
#9698=CIRCLE('',#26048,1.1);
#9699=CIRCLE('',#26052,1.1);
#11364=VERTEX_POINT('',#50262);
#11365=VERTEX_POINT('',#50263);
#11366=VERTEX_POINT('',#50265);
#11367=VERTEX_POINT('',#50291);
#11368=VERTEX_POINT('',#50334);
#11369=VERTEX_POINT('',#50335);
#11370=VERTEX_POINT('',#50421);
#11371=VERTEX_POINT('',#50422);
#11372=VERTEX_POINT('',#50511);
#11373=VERTEX_POINT('',#50512);
#11374=VERTEX_POINT('',#50598);
#11375=VERTEX_POINT('',#50599);
#11376=VERTEX_POINT('',#50688);
#11377=VERTEX_POINT('',#50689);
#11378=VERTEX_POINT('',#50775);
#11379=VERTEX_POINT('',#50776);
#11380=VERTEX_POINT('',#50862);
#11381=VERTEX_POINT('',#50863);
#11382=VERTEX_POINT('',#50952);
#11383=VERTEX_POINT('',#50953);
#11384=VERTEX_POINT('',#50955);
#11385=VERTEX_POINT('',#50968);
#11386=VERTEX_POINT('',#50969);
#11387=VERTEX_POINT('',#50971);
#11388=VERTEX_POINT('',#50979);
#11389=VERTEX_POINT('',#50994);
#11390=VERTEX_POINT('',#50995);
#11391=VERTEX_POINT('',#51031);
#11392=VERTEX_POINT('',#51032);
#11393=VERTEX_POINT('',#51068);
#11394=VERTEX_POINT('',#51069);
#11395=VERTEX_POINT('',#51106);
#11396=VERTEX_POINT('',#51107);
#11397=VERTEX_POINT('',#51143);
#11398=VERTEX_POINT('',#51144);
#11399=VERTEX_POINT('',#51180);
#11400=VERTEX_POINT('',#51181);
#11401=VERTEX_POINT('',#51218);
#11402=VERTEX_POINT('',#51219);
#11403=VERTEX_POINT('',#51256);
#11404=VERTEX_POINT('',#51257);
#11405=VERTEX_POINT('',#51259);
#11406=VERTEX_POINT('',#51265);
#11407=VERTEX_POINT('',#52329);
#11408=VERTEX_POINT('',#52421);
#11409=VERTEX_POINT('',#52422);
#11410=VERTEX_POINT('',#52426);
#11411=VERTEX_POINT('',#52428);
#11412=VERTEX_POINT('',#52430);
#11413=VERTEX_POINT('',#52433);
#11414=VERTEX_POINT('',#52437);
#11415=VERTEX_POINT('',#52441);
#11416=VERTEX_POINT('',#52445);
#11417=VERTEX_POINT('',#52446);
#11418=VERTEX_POINT('',#52452);
#11419=VERTEX_POINT('',#52457);
#14190=EDGE_CURVE('',#11364,#11365,#7079,.T.);
#14191=EDGE_CURVE('',#11365,#11366,#1069,.T.);
#14192=EDGE_CURVE('',#11366,#11367,#9685,.F.);
#14193=EDGE_CURVE('',#11367,#11364,#1070,.T.);
#14194=EDGE_CURVE('',#11368,#11369,#7080,.T.);
#14195=EDGE_CURVE('',#11369,#11365,#1071,.T.);
#14196=EDGE_CURVE('',#11364,#11368,#1072,.T.);
#14197=EDGE_CURVE('',#11370,#11371,#7081,.T.);
#14198=EDGE_CURVE('',#11371,#11369,#1073,.T.);
#14199=EDGE_CURVE('',#11368,#11370,#1074,.T.);
#14200=EDGE_CURVE('',#11372,#11373,#7082,.T.);
#14201=EDGE_CURVE('',#11373,#11371,#1075,.T.);
#14202=EDGE_CURVE('',#11370,#11372,#1076,.T.);
#14203=EDGE_CURVE('',#11374,#11375,#7083,.T.);
#14204=EDGE_CURVE('',#11375,#11373,#1077,.T.);
#14205=EDGE_CURVE('',#11372,#11374,#1078,.T.);
#14206=EDGE_CURVE('',#11376,#11377,#7084,.T.);
#14207=EDGE_CURVE('',#11377,#11375,#1079,.T.);
#14208=EDGE_CURVE('',#11374,#11376,#1080,.T.);
#14209=EDGE_CURVE('',#11378,#11379,#7085,.T.);
#14210=EDGE_CURVE('',#11379,#11377,#1081,.T.);
#14211=EDGE_CURVE('',#11376,#11378,#1082,.T.);
#14212=EDGE_CURVE('',#11380,#11381,#7086,.T.);
#14213=EDGE_CURVE('',#11381,#11379,#1083,.T.);
#14214=EDGE_CURVE('',#11378,#11380,#1084,.T.);
#14215=EDGE_CURVE('',#11382,#11383,#7087,.T.);
#14216=EDGE_CURVE('',#11384,#11382,#9686,.F.);
#14217=EDGE_CURVE('',#11384,#11383,#1085,.T.);
#14218=EDGE_CURVE('',#11385,#11386,#7088,.T.);
#14219=EDGE_CURVE('',#11386,#11387,#1086,.T.);
#14220=EDGE_CURVE('',#11388,#11387,#9687,.T.);
#14221=EDGE_CURVE('',#11385,#11388,#1087,.T.);
#14222=EDGE_CURVE('',#11389,#11390,#7089,.T.);
#14223=EDGE_CURVE('',#11390,#11386,#1088,.T.);
#14224=EDGE_CURVE('',#11389,#11385,#1089,.T.);
#14225=EDGE_CURVE('',#11391,#11392,#7090,.T.);
#14226=EDGE_CURVE('',#11392,#11390,#1090,.T.);
#14227=EDGE_CURVE('',#11391,#11389,#1091,.T.);
#14228=EDGE_CURVE('',#11393,#11394,#7091,.T.);
#14229=EDGE_CURVE('',#11394,#11392,#1092,.T.);
#14230=EDGE_CURVE('',#11393,#11391,#1093,.T.);
#14231=EDGE_CURVE('',#11395,#11396,#7092,.T.);
#14232=EDGE_CURVE('',#11396,#11394,#1094,.T.);
#14233=EDGE_CURVE('',#11395,#11393,#1095,.T.);
#14234=EDGE_CURVE('',#11397,#11398,#7093,.T.);
#14235=EDGE_CURVE('',#11398,#11396,#1096,.T.);
#14236=EDGE_CURVE('',#11397,#11395,#1097,.T.);
#14237=EDGE_CURVE('',#11399,#11400,#7094,.T.);
#14238=EDGE_CURVE('',#11400,#11398,#1098,.T.);
#14239=EDGE_CURVE('',#11399,#11397,#1099,.T.);
#14240=EDGE_CURVE('',#11401,#11402,#7095,.T.);
#14241=EDGE_CURVE('',#11402,#11400,#1100,.T.);
#14242=EDGE_CURVE('',#11401,#11399,#1101,.T.);
#14243=EDGE_CURVE('',#11403,#11404,#7096,.T.);
#14244=EDGE_CURVE('',#11405,#11403,#1102,.T.);
#14245=EDGE_CURVE('',#11406,#11405,#9688,.T.);
#14246=EDGE_CURVE('',#11406,#11404,#1103,.T.);
#14247=EDGE_CURVE('',#11404,#11402,#1104,.T.);
#14248=EDGE_CURVE('',#11403,#11401,#1105,.T.);
#14249=EDGE_CURVE('',#11387,#11384,#1106,.T.);
#14250=EDGE_CURVE('',#11366,#11406,#1107,.T.);
#14251=EDGE_CURVE('',#11383,#11381,#1108,.T.);
#14252=EDGE_CURVE('',#11407,#11388,#1109,.T.);
#14253=EDGE_CURVE('',#11380,#11407,#1110,.T.);
#14254=EDGE_CURVE('',#11405,#11367,#1111,.T.);
#14255=EDGE_CURVE('',#11408,#11409,#7097,.T.);
#14256=EDGE_CURVE('',#11409,#11408,#9689,.T.);
#14257=EDGE_CURVE('',#11382,#11407,#9690,.F.);
#14258=EDGE_CURVE('',#11410,#11410,#9691,.T.);
#14259=EDGE_CURVE('',#11411,#11411,#9692,.T.);
#14260=EDGE_CURVE('',#11412,#11412,#9693,.T.);
#14261=EDGE_CURVE('',#11413,#11413,#9694,.T.);
#14262=EDGE_CURVE('',#11413,#11412,#7098,.T.);
#14263=EDGE_CURVE('',#11414,#11414,#9695,.T.);
#14264=EDGE_CURVE('',#11414,#11411,#7099,.T.);
#14265=EDGE_CURVE('',#11415,#11415,#9696,.T.);
#14266=EDGE_CURVE('',#11415,#11410,#7100,.T.);
#14267=EDGE_CURVE('',#11416,#11417,#7101,.T.);
#14268=EDGE_CURVE('',#11409,#11416,#7102,.T.);
#14269=EDGE_CURVE('',#11417,#11408,#7103,.T.);
#14270=EDGE_CURVE('',#11416,#11417,#9697,.T.);
#14271=EDGE_CURVE('',#11418,#11418,#9698,.T.);
#14272=EDGE_CURVE('',#11418,#11419,#7104,.T.);
#14273=EDGE_CURVE('',#11419,#11419,#9699,.T.);
#19612=ORIENTED_EDGE('',*,*,#14190,.T.);
#19613=ORIENTED_EDGE('',*,*,#14191,.T.);
#19614=ORIENTED_EDGE('',*,*,#14192,.T.);
#19615=ORIENTED_EDGE('',*,*,#14193,.T.);
#19616=ORIENTED_EDGE('',*,*,#14194,.T.);
#19617=ORIENTED_EDGE('',*,*,#14195,.T.);
#19618=ORIENTED_EDGE('',*,*,#14190,.F.);
#19619=ORIENTED_EDGE('',*,*,#14196,.T.);
#19620=ORIENTED_EDGE('',*,*,#14197,.T.);
#19621=ORIENTED_EDGE('',*,*,#14198,.T.);
#19622=ORIENTED_EDGE('',*,*,#14194,.F.);
#19623=ORIENTED_EDGE('',*,*,#14199,.T.);
#19624=ORIENTED_EDGE('',*,*,#14200,.T.);
#19625=ORIENTED_EDGE('',*,*,#14201,.T.);
#19626=ORIENTED_EDGE('',*,*,#14197,.F.);
#19627=ORIENTED_EDGE('',*,*,#14202,.T.);
#19628=ORIENTED_EDGE('',*,*,#14203,.T.);
#19629=ORIENTED_EDGE('',*,*,#14204,.T.);
#19630=ORIENTED_EDGE('',*,*,#14200,.F.);
#19631=ORIENTED_EDGE('',*,*,#14205,.T.);
#19632=ORIENTED_EDGE('',*,*,#14206,.T.);
#19633=ORIENTED_EDGE('',*,*,#14207,.T.);
#19634=ORIENTED_EDGE('',*,*,#14203,.F.);
#19635=ORIENTED_EDGE('',*,*,#14208,.T.);
#19636=ORIENTED_EDGE('',*,*,#14209,.T.);
#19637=ORIENTED_EDGE('',*,*,#14210,.T.);
#19638=ORIENTED_EDGE('',*,*,#14206,.F.);
#19639=ORIENTED_EDGE('',*,*,#14211,.T.);
#19640=ORIENTED_EDGE('',*,*,#14212,.T.);
#19641=ORIENTED_EDGE('',*,*,#14213,.T.);
#19642=ORIENTED_EDGE('',*,*,#14209,.F.);
#19643=ORIENTED_EDGE('',*,*,#14214,.T.);
#19644=ORIENTED_EDGE('',*,*,#14215,.F.);
#19645=ORIENTED_EDGE('',*,*,#14216,.F.);
#19646=ORIENTED_EDGE('',*,*,#14217,.T.);
#19647=ORIENTED_EDGE('',*,*,#14218,.T.);
#19648=ORIENTED_EDGE('',*,*,#14219,.T.);
#19649=ORIENTED_EDGE('',*,*,#14220,.F.);
#19650=ORIENTED_EDGE('',*,*,#14221,.F.);
#19651=ORIENTED_EDGE('',*,*,#14222,.T.);
#19652=ORIENTED_EDGE('',*,*,#14223,.T.);
#19653=ORIENTED_EDGE('',*,*,#14218,.F.);
#19654=ORIENTED_EDGE('',*,*,#14224,.F.);
#19655=ORIENTED_EDGE('',*,*,#14225,.T.);
#19656=ORIENTED_EDGE('',*,*,#14226,.T.);
#19657=ORIENTED_EDGE('',*,*,#14222,.F.);
#19658=ORIENTED_EDGE('',*,*,#14227,.F.);
#19659=ORIENTED_EDGE('',*,*,#14228,.T.);
#19660=ORIENTED_EDGE('',*,*,#14229,.T.);
#19661=ORIENTED_EDGE('',*,*,#14225,.F.);
#19662=ORIENTED_EDGE('',*,*,#14230,.F.);
#19663=ORIENTED_EDGE('',*,*,#14231,.T.);
#19664=ORIENTED_EDGE('',*,*,#14232,.T.);
#19665=ORIENTED_EDGE('',*,*,#14228,.F.);
#19666=ORIENTED_EDGE('',*,*,#14233,.F.);
#19667=ORIENTED_EDGE('',*,*,#14234,.T.);
#19668=ORIENTED_EDGE('',*,*,#14235,.T.);
#19669=ORIENTED_EDGE('',*,*,#14231,.F.);
#19670=ORIENTED_EDGE('',*,*,#14236,.F.);
#19671=ORIENTED_EDGE('',*,*,#14237,.T.);
#19672=ORIENTED_EDGE('',*,*,#14238,.T.);
#19673=ORIENTED_EDGE('',*,*,#14234,.F.);
#19674=ORIENTED_EDGE('',*,*,#14239,.F.);
#19675=ORIENTED_EDGE('',*,*,#14240,.T.);
#19676=ORIENTED_EDGE('',*,*,#14241,.T.);
#19677=ORIENTED_EDGE('',*,*,#14237,.F.);
#19678=ORIENTED_EDGE('',*,*,#14242,.F.);
#19679=ORIENTED_EDGE('',*,*,#14243,.F.);
#19680=ORIENTED_EDGE('',*,*,#14244,.F.);
#19681=ORIENTED_EDGE('',*,*,#14245,.F.);
#19682=ORIENTED_EDGE('',*,*,#14246,.T.);
#19683=ORIENTED_EDGE('',*,*,#14243,.T.);
#19684=ORIENTED_EDGE('',*,*,#14247,.T.);
#19685=ORIENTED_EDGE('',*,*,#14240,.F.);
#19686=ORIENTED_EDGE('',*,*,#14248,.F.);
#19687=ORIENTED_EDGE('',*,*,#14249,.F.);
#19688=ORIENTED_EDGE('',*,*,#14219,.F.);
#19689=ORIENTED_EDGE('',*,*,#14223,.F.);
#19690=ORIENTED_EDGE('',*,*,#14226,.F.);
#19691=ORIENTED_EDGE('',*,*,#14229,.F.);
#19692=ORIENTED_EDGE('',*,*,#14232,.F.);
#19693=ORIENTED_EDGE('',*,*,#14235,.F.);
#19694=ORIENTED_EDGE('',*,*,#14238,.F.);
#19695=ORIENTED_EDGE('',*,*,#14241,.F.);
#19696=ORIENTED_EDGE('',*,*,#14247,.F.);
#19697=ORIENTED_EDGE('',*,*,#14246,.F.);
#19698=ORIENTED_EDGE('',*,*,#14250,.F.);
#19699=ORIENTED_EDGE('',*,*,#14191,.F.);
#19700=ORIENTED_EDGE('',*,*,#14195,.F.);
#19701=ORIENTED_EDGE('',*,*,#14198,.F.);
#19702=ORIENTED_EDGE('',*,*,#14201,.F.);
#19703=ORIENTED_EDGE('',*,*,#14204,.F.);
#19704=ORIENTED_EDGE('',*,*,#14207,.F.);
#19705=ORIENTED_EDGE('',*,*,#14210,.F.);
#19706=ORIENTED_EDGE('',*,*,#14213,.F.);
#19707=ORIENTED_EDGE('',*,*,#14251,.F.);
#19708=ORIENTED_EDGE('',*,*,#14217,.F.);
#19709=ORIENTED_EDGE('',*,*,#14252,.F.);
#19710=ORIENTED_EDGE('',*,*,#14253,.F.);
#19711=ORIENTED_EDGE('',*,*,#14214,.F.);
#19712=ORIENTED_EDGE('',*,*,#14211,.F.);
#19713=ORIENTED_EDGE('',*,*,#14208,.F.);
#19714=ORIENTED_EDGE('',*,*,#14205,.F.);
#19715=ORIENTED_EDGE('',*,*,#14202,.F.);
#19716=ORIENTED_EDGE('',*,*,#14199,.F.);
#19717=ORIENTED_EDGE('',*,*,#14196,.F.);
#19718=ORIENTED_EDGE('',*,*,#14193,.F.);
#19719=ORIENTED_EDGE('',*,*,#14254,.F.);
#19720=ORIENTED_EDGE('',*,*,#14244,.T.);
#19721=ORIENTED_EDGE('',*,*,#14248,.T.);
#19722=ORIENTED_EDGE('',*,*,#14242,.T.);
#19723=ORIENTED_EDGE('',*,*,#14239,.T.);
#19724=ORIENTED_EDGE('',*,*,#14236,.T.);
#19725=ORIENTED_EDGE('',*,*,#14233,.T.);
#19726=ORIENTED_EDGE('',*,*,#14230,.T.);
#19727=ORIENTED_EDGE('',*,*,#14227,.T.);
#19728=ORIENTED_EDGE('',*,*,#14224,.T.);
#19729=ORIENTED_EDGE('',*,*,#14221,.T.);
#19730=ORIENTED_EDGE('',*,*,#14255,.T.);
#19731=ORIENTED_EDGE('',*,*,#14256,.T.);
#19732=ORIENTED_EDGE('',*,*,#14252,.T.);
#19733=ORIENTED_EDGE('',*,*,#14220,.T.);
#19734=ORIENTED_EDGE('',*,*,#14249,.T.);
#19735=ORIENTED_EDGE('',*,*,#14216,.T.);
#19736=ORIENTED_EDGE('',*,*,#14257,.T.);
#19737=ORIENTED_EDGE('',*,*,#14258,.T.);
#19738=ORIENTED_EDGE('',*,*,#14259,.T.);
#19739=ORIENTED_EDGE('',*,*,#14260,.T.);
#19740=ORIENTED_EDGE('',*,*,#14261,.F.);
#19741=ORIENTED_EDGE('',*,*,#14262,.T.);
#19742=ORIENTED_EDGE('',*,*,#14260,.F.);
#19743=ORIENTED_EDGE('',*,*,#14262,.F.);
#19744=ORIENTED_EDGE('',*,*,#14263,.F.);
#19745=ORIENTED_EDGE('',*,*,#14264,.T.);
#19746=ORIENTED_EDGE('',*,*,#14259,.F.);
#19747=ORIENTED_EDGE('',*,*,#14264,.F.);
#19748=ORIENTED_EDGE('',*,*,#14265,.F.);
#19749=ORIENTED_EDGE('',*,*,#14266,.T.);
#19750=ORIENTED_EDGE('',*,*,#14258,.F.);
#19751=ORIENTED_EDGE('',*,*,#14266,.F.);
#19752=ORIENTED_EDGE('',*,*,#14267,.F.);
#19753=ORIENTED_EDGE('',*,*,#14268,.F.);
#19754=ORIENTED_EDGE('',*,*,#14255,.F.);
#19755=ORIENTED_EDGE('',*,*,#14269,.F.);
#19756=ORIENTED_EDGE('',*,*,#14267,.T.);
#19757=ORIENTED_EDGE('',*,*,#14270,.F.);
#19758=ORIENTED_EDGE('',*,*,#14261,.T.);
#19759=ORIENTED_EDGE('',*,*,#14263,.T.);
#19760=ORIENTED_EDGE('',*,*,#14265,.T.);
#19761=ORIENTED_EDGE('',*,*,#14271,.T.);
#19762=ORIENTED_EDGE('',*,*,#14269,.T.);
#19763=ORIENTED_EDGE('',*,*,#14256,.F.);
#19764=ORIENTED_EDGE('',*,*,#14268,.T.);
#19765=ORIENTED_EDGE('',*,*,#14270,.T.);
#19766=ORIENTED_EDGE('',*,*,#14215,.T.);
#19767=ORIENTED_EDGE('',*,*,#14251,.T.);
#19768=ORIENTED_EDGE('',*,*,#14212,.F.);
#19769=ORIENTED_EDGE('',*,*,#14253,.T.);
#19770=ORIENTED_EDGE('',*,*,#14257,.F.);
#19771=ORIENTED_EDGE('',*,*,#14271,.F.);
#19772=ORIENTED_EDGE('',*,*,#14272,.T.);
#19773=ORIENTED_EDGE('',*,*,#14273,.T.);
#19774=ORIENTED_EDGE('',*,*,#14272,.F.);
#19775=ORIENTED_EDGE('',*,*,#14273,.F.);
#19776=ORIENTED_EDGE('',*,*,#14254,.T.);
#19777=ORIENTED_EDGE('',*,*,#14192,.F.);
#19778=ORIENTED_EDGE('',*,*,#14250,.T.);
#19779=ORIENTED_EDGE('',*,*,#14245,.T.);
#21471=CYLINDRICAL_SURFACE('',#26010,0.457875);
#21472=CYLINDRICAL_SURFACE('',#26012,0.457875);
#21473=CYLINDRICAL_SURFACE('',#26013,0.457875);
#21474=CYLINDRICAL_SURFACE('',#26014,0.457875);
#21475=CYLINDRICAL_SURFACE('',#26015,0.457875);
#21476=CYLINDRICAL_SURFACE('',#26016,0.457875);
#21477=CYLINDRICAL_SURFACE('',#26017,0.457875);
#21478=CYLINDRICAL_SURFACE('',#26018,0.457875);
#21479=CYLINDRICAL_SURFACE('',#26019,0.457875);
#21480=CYLINDRICAL_SURFACE('',#26021,0.625);
#21481=CYLINDRICAL_SURFACE('',#26023,0.625);
#21482=CYLINDRICAL_SURFACE('',#26024,0.625);
#21483=CYLINDRICAL_SURFACE('',#26025,0.625);
#21484=CYLINDRICAL_SURFACE('',#26026,0.625);
#21485=CYLINDRICAL_SURFACE('',#26027,0.625);
#21486=CYLINDRICAL_SURFACE('',#26028,0.625);
#21487=CYLINDRICAL_SURFACE('',#26029,0.625);
#21488=CYLINDRICAL_SURFACE('',#26030,0.625);
#21489=CYLINDRICAL_SURFACE('',#26032,0.625);
#21490=CYLINDRICAL_SURFACE('',#26039,0.225);
#21491=CYLINDRICAL_SURFACE('',#26041,0.225);
#21492=CYLINDRICAL_SURFACE('',#26043,0.225);
#21493=CYLINDRICAL_SURFACE('',#26049,1.9);
#21494=CYLINDRICAL_SURFACE('',#26050,0.457875);
#21495=CYLINDRICAL_SURFACE('',#26051,1.1);
#22681=ADVANCED_FACE('',(#3900),#21471,.F.);
#22682=ADVANCED_FACE('',(#3901),#21472,.F.);
#22683=ADVANCED_FACE('',(#3902),#21473,.F.);
#22684=ADVANCED_FACE('',(#3903),#21474,.F.);
#22685=ADVANCED_FACE('',(#3904),#21475,.F.);
#22686=ADVANCED_FACE('',(#3905),#21476,.F.);
#22687=ADVANCED_FACE('',(#3906),#21477,.F.);
#22688=ADVANCED_FACE('',(#3907),#21478,.F.);
#22689=ADVANCED_FACE('',(#3908),#21479,.F.);
#22690=ADVANCED_FACE('',(#3909),#21480,.F.);
#22691=ADVANCED_FACE('',(#3910),#21481,.F.);
#22692=ADVANCED_FACE('',(#3911),#21482,.F.);
#22693=ADVANCED_FACE('',(#3912),#21483,.F.);
#22694=ADVANCED_FACE('',(#3913),#21484,.F.);
#22695=ADVANCED_FACE('',(#3914),#21485,.F.);
#22696=ADVANCED_FACE('',(#3915),#21486,.F.);
#22697=ADVANCED_FACE('',(#3916),#21487,.F.);
#22698=ADVANCED_FACE('',(#3917),#21488,.F.);
#22699=ADVANCED_FACE('',(#3918),#21489,.F.);
#22700=ADVANCED_FACE('',(#3919),#15,.F.);
#22701=ADVANCED_FACE('',(#3920),#16,.F.);
#22702=ADVANCED_FACE('',(#3921,#2261,#2262,#2263,#2264),#2783,.T.);
#22703=ADVANCED_FACE('',(#3922),#21490,.F.);
#22704=ADVANCED_FACE('',(#3923),#21491,.F.);
#22705=ADVANCED_FACE('',(#3924),#21492,.F.);
#22706=ADVANCED_FACE('',(#3925),#2784,.F.);
#22707=ADVANCED_FACE('',(#3926,#2265,#2266,#2267,#2268),#2785,.F.);
#22708=ADVANCED_FACE('',(#3927),#21493,.T.);
#22709=ADVANCED_FACE('',(#3928),#21494,.F.);
#22710=ADVANCED_FACE('',(#3929),#21495,.T.);
#22711=ADVANCED_FACE('',(#3930,#2269),#2786,.F.);
#23070=CLOSED_SHELL('',(#22681,#22682,#22683,#22684,#22685,#22686,#22687,
#22688,#22689,#22690,#22691,#22692,#22693,#22694,#22695,#22696,#22697,#22698,
#22699,#22700,#22701,#22702,#22703,#22704,#22705,#22706,#22707,#22708,#22709,
#22710,#22711));
#26009=AXIS2_PLACEMENT_3D('',#50260,#31652,#31653);
#26010=AXIS2_PLACEMENT_3D('',#50261,#31654,#31655);
#26011=AXIS2_PLACEMENT_3D('',#50292,#31657,#31658);
#26012=AXIS2_PLACEMENT_3D('',#50333,#31659,#31660);
#26013=AXIS2_PLACEMENT_3D('',#50420,#31662,#31663);
#26014=AXIS2_PLACEMENT_3D('',#50510,#31665,#31666);
#26015=AXIS2_PLACEMENT_3D('',#50597,#31668,#31669);
#26016=AXIS2_PLACEMENT_3D('',#50687,#31671,#31672);
#26017=AXIS2_PLACEMENT_3D('',#50774,#31674,#31675);
#26018=AXIS2_PLACEMENT_3D('',#50861,#31677,#31678);
#26019=AXIS2_PLACEMENT_3D('',#50951,#31680,#31681);
#26020=AXIS2_PLACEMENT_3D('',#50956,#31683,#31684);
#26021=AXIS2_PLACEMENT_3D('',#50967,#31685,#31686);
#26022=AXIS2_PLACEMENT_3D('',#50980,#31688,#31689);
#26023=AXIS2_PLACEMENT_3D('',#50993,#31690,#31691);
#26024=AXIS2_PLACEMENT_3D('',#51030,#31693,#31694);
#26025=AXIS2_PLACEMENT_3D('',#51067,#31696,#31697);
#26026=AXIS2_PLACEMENT_3D('',#51105,#31699,#31700);
#26027=AXIS2_PLACEMENT_3D('',#51142,#31702,#31703);
#26028=AXIS2_PLACEMENT_3D('',#51179,#31705,#31706);
#26029=AXIS2_PLACEMENT_3D('',#51217,#31708,#31709);
#26030=AXIS2_PLACEMENT_3D('',#51255,#31711,#31712);
#26031=AXIS2_PLACEMENT_3D('',#51266,#31714,#31715);
#26032=AXIS2_PLACEMENT_3D('',#51277,#31716,#31717);
#26033=AXIS2_PLACEMENT_3D('',#52420,#31718,#31719);
#26034=AXIS2_PLACEMENT_3D('',#52424,#31721,#31722);
#26035=AXIS2_PLACEMENT_3D('',#52425,#31723,#31724);
#26036=AXIS2_PLACEMENT_3D('',#52427,#31725,#31726);
#26037=AXIS2_PLACEMENT_3D('',#52429,#31727,#31728);
#26038=AXIS2_PLACEMENT_3D('',#52431,#31729,#31730);
#26039=AXIS2_PLACEMENT_3D('',#52432,#31731,#31732);
#26040=AXIS2_PLACEMENT_3D('',#52434,#31733,#31734);
#26041=AXIS2_PLACEMENT_3D('',#52436,#31736,#31737);
#26042=AXIS2_PLACEMENT_3D('',#52438,#31738,#31739);
#26043=AXIS2_PLACEMENT_3D('',#52440,#31741,#31742);
#26044=AXIS2_PLACEMENT_3D('',#52442,#31743,#31744);
#26045=AXIS2_PLACEMENT_3D('',#52444,#31746,#31747);
#26046=AXIS2_PLACEMENT_3D('',#52450,#31751,#31752);
#26047=AXIS2_PLACEMENT_3D('',#52451,#31753,#31754);
#26048=AXIS2_PLACEMENT_3D('',#52453,#31755,#31756);
#26049=AXIS2_PLACEMENT_3D('',#52454,#31757,#31758);
#26050=AXIS2_PLACEMENT_3D('',#52455,#31759,#31760);
#26051=AXIS2_PLACEMENT_3D('',#52456,#31761,#31762);
#26052=AXIS2_PLACEMENT_3D('',#52459,#31764,#31765);
#26053=AXIS2_PLACEMENT_3D('',#52460,#31766,#31767);
#31652=DIRECTION('axis',(0.,0.,1.));
#31653=DIRECTION('refdir',(1.,0.,0.));
#31654=DIRECTION('center_axis',(1.,0.,0.));
#31655=DIRECTION('ref_axis',(0.,0.207879895528894,-0.978154358490978));
#31656=DIRECTION('',(-1.,0.,0.));
#31657=DIRECTION('center_axis',(1.,0.,0.));
#31658=DIRECTION('ref_axis',(0.,0.,-1.));
#31659=DIRECTION('center_axis',(1.,0.,0.));
#31660=DIRECTION('ref_axis',(0.,0.,-1.));
#31661=DIRECTION('',(-1.,0.,0.));
#31662=DIRECTION('center_axis',(1.,0.,0.));
#31663=DIRECTION('ref_axis',(0.,0.,-1.));
#31664=DIRECTION('',(-1.,0.,0.));
#31665=DIRECTION('center_axis',(1.,0.,0.));
#31666=DIRECTION('ref_axis',(0.,0.,-1.));
#31667=DIRECTION('',(-1.,0.,0.));
#31668=DIRECTION('center_axis',(1.,0.,0.));
#31669=DIRECTION('ref_axis',(0.,0.,-1.));
#31670=DIRECTION('',(-1.,0.,0.));
#31671=DIRECTION('center_axis',(1.,0.,0.));
#31672=DIRECTION('ref_axis',(0.,0.,-1.));
#31673=DIRECTION('',(-1.,0.,0.));
#31674=DIRECTION('center_axis',(1.,0.,0.));
#31675=DIRECTION('ref_axis',(0.,0.,-1.));
#31676=DIRECTION('',(-1.,0.,0.));
#31677=DIRECTION('center_axis',(1.,0.,0.));
#31678=DIRECTION('ref_axis',(0.,0.,-1.));
#31679=DIRECTION('',(-1.,0.,0.));
#31680=DIRECTION('center_axis',(1.,0.,0.));
#31681=DIRECTION('ref_axis',(0.,0.,-1.));
#31682=DIRECTION('',(-1.,0.,0.));
#31683=DIRECTION('center_axis',(1.,0.,0.));
#31684=DIRECTION('ref_axis',(0.,0.,-1.));
#31685=DIRECTION('center_axis',(1.,0.,0.));
#31686=DIRECTION('ref_axis',(0.,2.68771689099506E-14,-1.));
#31687=DIRECTION('',(1.,3.30650148539799E-30,-1.22464679914735E-16));
#31688=DIRECTION('center_axis',(-1.,0.,0.));
#31689=DIRECTION('ref_axis',(0.,2.68771689099506E-14,-1.));
#31690=DIRECTION('center_axis',(1.,0.,0.));
#31691=DIRECTION('ref_axis',(0.,2.68771689099506E-14,-1.));
#31692=DIRECTION('',(1.,3.30650148539799E-30,-1.22464679914735E-16));
#31693=DIRECTION('center_axis',(1.,0.,0.));
#31694=DIRECTION('ref_axis',(0.,2.68771689099506E-14,-1.));
#31695=DIRECTION('',(1.,3.30650148539799E-30,-1.22464679914735E-16));
#31696=DIRECTION('center_axis',(1.,0.,0.));
#31697=DIRECTION('ref_axis',(0.,2.68771689099506E-14,-1.));
#31698=DIRECTION('',(1.,3.30650148539799E-30,-1.22464679914735E-16));
#31699=DIRECTION('center_axis',(1.,0.,0.));
#31700=DIRECTION('ref_axis',(0.,2.68771689099506E-14,-1.));
#31701=DIRECTION('',(1.,3.30650148539799E-30,-1.22464679914735E-16));
#31702=DIRECTION('center_axis',(1.,0.,0.));
#31703=DIRECTION('ref_axis',(0.,2.68771689099506E-14,-1.));
#31704=DIRECTION('',(1.,3.30650148539799E-30,-1.22464679914735E-16));
#31705=DIRECTION('center_axis',(1.,0.,0.));
#31706=DIRECTION('ref_axis',(0.,2.68771689099506E-14,-1.));
#31707=DIRECTION('',(1.,3.30650148539799E-30,-1.22464679914735E-16));
#31708=DIRECTION('center_axis',(1.,0.,0.));
#31709=DIRECTION('ref_axis',(0.,2.68771689099506E-14,-1.));
#31710=DIRECTION('',(1.,3.30650148539799E-30,-1.22464679914735E-16));
#31711=DIRECTION('center_axis',(1.,0.,0.));
#31712=DIRECTION('ref_axis',(0.,2.68771689099506E-14,-1.));
#31713=DIRECTION('',(1.,3.30650148539799E-30,-1.22464679914735E-16));
#31714=DIRECTION('center_axis',(1.,0.,0.));
#31715=DIRECTION('ref_axis',(0.,2.68771689099506E-14,-1.));
#31716=DIRECTION('center_axis',(1.,0.,0.));
#31717=DIRECTION('ref_axis',(0.,2.68771689099506E-14,-1.));
#31718=DIRECTION('center_axis',(1.,0.,0.));
#31719=DIRECTION('ref_axis',(0.,0.,-1.));
#31720=DIRECTION('',(0.,1.,0.));
#31721=DIRECTION('center_axis',(1.,0.,0.));
#31722=DIRECTION('ref_axis',(0.,0.,-1.));
#31723=DIRECTION('center_axis',(1.,0.,0.));
#31724=DIRECTION('ref_axis',(0.,0.,-1.));
#31725=DIRECTION('center_axis',(-1.,0.,0.));
#31726=DIRECTION('ref_axis',(0.,0.,-1.));
#31727=DIRECTION('center_axis',(-1.,0.,0.));
#31728=DIRECTION('ref_axis',(0.,0.,-1.));
#31729=DIRECTION('center_axis',(-1.,0.,0.));
#31730=DIRECTION('ref_axis',(0.,0.,-1.));
#31731=DIRECTION('center_axis',(1.,0.,0.));
#31732=DIRECTION('ref_axis',(0.,0.,-1.));
#31733=DIRECTION('center_axis',(1.,0.,0.));
#31734=DIRECTION('ref_axis',(0.,0.,-1.));
#31735=DIRECTION('',(1.,0.,0.));
#31736=DIRECTION('center_axis',(1.,0.,0.));
#31737=DIRECTION('ref_axis',(0.,0.,-1.));
#31738=DIRECTION('center_axis',(1.,0.,0.));
#31739=DIRECTION('ref_axis',(0.,0.,-1.));
#31740=DIRECTION('',(1.,0.,0.));
#31741=DIRECTION('center_axis',(1.,0.,0.));
#31742=DIRECTION('ref_axis',(0.,0.,-1.));
#31743=DIRECTION('center_axis',(1.,0.,0.));
#31744=DIRECTION('ref_axis',(0.,0.,-1.));
#31745=DIRECTION('',(1.,0.,0.));
#31746=DIRECTION('center_axis',(0.,0.,1.));
#31747=DIRECTION('ref_axis',(0.,-1.,0.));
#31748=DIRECTION('',(0.,-1.,0.));
#31749=DIRECTION('',(-1.,0.,0.));
#31750=DIRECTION('',(1.,0.,0.));
#31751=DIRECTION('center_axis',(1.,0.,0.));
#31752=DIRECTION('ref_axis',(0.,0.,-1.));
#31753=DIRECTION('center_axis',(1.,0.,0.));
#31754=DIRECTION('ref_axis',(0.,0.,-1.));
#31755=DIRECTION('center_axis',(1.,0.,0.));
#31756=DIRECTION('ref_axis',(0.,0.,-1.));
#31757=DIRECTION('center_axis',(1.,0.,0.));
#31758=DIRECTION('ref_axis',(0.,-1.22464679914735E-16,1.));
#31759=DIRECTION('center_axis',(1.,0.,0.));
#31760=DIRECTION('ref_axis',(0.,0.,-1.));
#31761=DIRECTION('center_axis',(1.,0.,0.));
#31762=DIRECTION('ref_axis',(0.,0.,-1.));
#31763=DIRECTION('',(-1.,0.,0.));
#31764=DIRECTION('center_axis',(1.,0.,0.));
#31765=DIRECTION('ref_axis',(0.,0.,-1.));
#31766=DIRECTION('center_axis',(1.,0.,0.));
#31767=DIRECTION('ref_axis',(0.,0.,-1.));
#50260=CARTESIAN_POINT('',(0.,0.,0.));
#50261=CARTESIAN_POINT('Origin',(12.5,0.,4.));
#50262=CARTESIAN_POINT('',(12.7800042915148,-1.13874042544416E-5,4.45787212683272));
#50263=CARTESIAN_POINT('',(12.6699957084852,1.09516003635735E-5,4.45788309353564));
#50264=CARTESIAN_POINT('',(12.5,-5.60735153159594E-17,4.457875));
#50265=CARTESIAN_POINT('',(12.5,-0.186196943290586,3.58169363627331));
#50266=CARTESIAN_POINT('Ctrl Pts',(12.6699957084852,1.09516003635735E-5,
4.45788309353564));
#50267=CARTESIAN_POINT('Ctrl Pts',(12.6684300766731,0.0150239422001319,
4.45789815019349));
#50268=CARTESIAN_POINT('Ctrl Pts',(12.6668644448611,0.0300354905662504,
4.45717403092565));
#50269=CARTESIAN_POINT('Ctrl Pts',(12.6652988130491,0.0449730203321769,
4.45569984746698));
#50270=CARTESIAN_POINT('Ctrl Pts',(12.6574274409991,0.120072959788606,4.44828824124903));
#50271=CARTESIAN_POINT('Ctrl Pts',(12.6495560689492,0.193301947984492,4.42191743369942));
#50272=CARTESIAN_POINT('Ctrl Pts',(12.6416846968992,0.255884660534875,4.37974732787395));
#50273=CARTESIAN_POINT('Ctrl Pts',(12.6338133248492,0.318467373085258,4.33757722204849));
#50274=CARTESIAN_POINT('Ctrl Pts',(12.6259419527993,0.370403809990138,4.27960781794716));
#50275=CARTESIAN_POINT('Ctrl Pts',(12.6180705807493,0.405471379329245,4.2127856577826));
#50276=CARTESIAN_POINT('Ctrl Pts',(12.6101992086994,0.440538948668352,4.14596349761803));
#50277=CARTESIAN_POINT('Ctrl Pts',(12.6023278366494,0.458737650441686,4.07028858139023));
#50278=CARTESIAN_POINT('Ctrl Pts',(12.5944564645995,0.457884906392306,3.99482861029462));
#50279=CARTESIAN_POINT('Ctrl Pts',(12.5865850925495,0.457032162342926,3.91936863919901));
#50280=CARTESIAN_POINT('Ctrl Pts',(12.5787137204996,0.437127972470831,3.84412361323559));
#50281=CARTESIAN_POINT('Ctrl Pts',(12.5708423484496,0.400561475243013,3.77811083326841));
#50282=CARTESIAN_POINT('Ctrl Pts',(12.5629709763996,0.363994978015195,3.71209805330123));
#50283=CARTESIAN_POINT('Ctrl Pts',(12.5550996043497,0.310766173431653,3.6553175193303));
#50284=CARTESIAN_POINT('Ctrl Pts',(12.5472282322997,0.247245050961511,3.61457214242492));
#50285=CARTESIAN_POINT('Ctrl Pts',(12.5393568602498,0.183723928491369,3.57382676551955));
#50286=CARTESIAN_POINT('Ctrl Pts',(12.5314854881998,0.109910488134627,3.54911654567973));
#50287=CARTESIAN_POINT('Ctrl Pts',(12.5236141161499,0.034670519197381,3.5434092666393));
#50288=CARTESIAN_POINT('Ctrl Pts',(12.5157427440999,-0.0405694497398647,
3.53770198759887));
#50289=CARTESIAN_POINT('Ctrl Pts',(12.50787137205,-0.117235947257613,3.55099764935784));
#50290=CARTESIAN_POINT('Ctrl Pts',(12.5,-0.186196943290592,3.58169363627332));
#50291=CARTESIAN_POINT('',(12.5,-0.186217277007329,4.41832740439831));
#50292=CARTESIAN_POINT('Origin',(12.5,0.,4.));
#50293=CARTESIAN_POINT('Ctrl Pts',(12.5,-0.186217277007329,4.41832740439831));
#50294=CARTESIAN_POINT('Ctrl Pts',(12.5008157411716,-0.193365324225124,
4.41515241707318));
#50295=CARTESIAN_POINT('Ctrl Pts',(12.5016314823431,-0.200430783441492,
4.4117927098014));
#50296=CARTESIAN_POINT('Ctrl Pts',(12.5024472235147,-0.207403505574881,
4.40825058102053));
#50297=CARTESIAN_POINT('Ctrl Pts',(12.5103185955646,-0.274685741688951,
4.37407134077235));
#50298=CARTESIAN_POINT('Ctrl Pts',(12.5181899676146,-0.333333232193243,
4.32290684204764));
#50299=CARTESIAN_POINT('Ctrl Pts',(12.5260613396645,-0.376326743005614,
4.26088786252735));
#50300=CARTESIAN_POINT('Ctrl Pts',(12.5339327117145,-0.419320253817985,
4.19886888300706));
#50301=CARTESIAN_POINT('Ctrl Pts',(12.5418040837645,-0.446659784938435,
4.12599542269119));
#50302=CARTESIAN_POINT('Ctrl Pts',(12.5496754558144,-0.455065168373522,
4.05100019606997));
#50303=CARTESIAN_POINT('Ctrl Pts',(12.5575468278644,-0.463470551808608,
3.97600496944875));
#50304=CARTESIAN_POINT('Ctrl Pts',(12.5654181999143,-0.452941787558331,
3.89888797652218));
#50305=CARTESIAN_POINT('Ctrl Pts',(12.5732895719643,-0.424742400952558,
3.82888990513641));
#50306=CARTESIAN_POINT('Ctrl Pts',(12.5811609440142,-0.396543014346786,
3.75889183375065));
#50307=CARTESIAN_POINT('Ctrl Pts',(12.5890323160642,-0.350673005385519,
3.69601268390568));
#50308=CARTESIAN_POINT('Ctrl Pts',(12.5969036881141,-0.292628022669152,
3.64778723809593));
#50309=CARTESIAN_POINT('Ctrl Pts',(12.6047750601641,-0.234583039952784,
3.59956179228618));
#50310=CARTESIAN_POINT('Ctrl Pts',(12.6126464322141,-0.164363083481316,
3.56599005051166));
#50311=CARTESIAN_POINT('Ctrl Pts',(12.620517804264,-0.0903829156297007,
3.55109483330951));
#50312=CARTESIAN_POINT('Ctrl Pts',(12.628389176314,-0.0164027477780855,
3.53619961610736));
#50313=CARTESIAN_POINT('Ctrl Pts',(12.6362605483639,0.0613376314536766,
3.53998092347757));
#50314=CARTESIAN_POINT('Ctrl Pts',(12.6441319204139,0.13352290298843,3.56198566164487));
#50315=CARTESIAN_POINT('Ctrl Pts',(12.6520032924638,0.205708174523184,3.58399039981218));
#50316=CARTESIAN_POINT('Ctrl Pts',(12.6598746645138,0.272338338360929,3.62421856877658));
#50317=CARTESIAN_POINT('Ctrl Pts',(12.6677460365637,0.325429113408527,3.67784968145944));
#50318=CARTESIAN_POINT('Ctrl Pts',(12.6756174086137,0.378519888456125,3.7314807941423));
#50319=CARTESIAN_POINT('Ctrl Pts',(12.6834887806637,0.418071274713577,3.79851485054363));
#50320=CARTESIAN_POINT('Ctrl Pts',(12.6913601527136,0.439343931585728,3.87091926467948));
#50321=CARTESIAN_POINT('Ctrl Pts',(12.6992315247636,0.460616588457879,3.94332367881533));
#50322=CARTESIAN_POINT('Ctrl Pts',(12.7071028968135,0.46361051594473,4.02109845068571));
#50323=CARTESIAN_POINT('Ctrl Pts',(12.7149742688635,0.447966936692366,4.09492394607626));
#50324=CARTESIAN_POINT('Ctrl Pts',(12.7228456409134,0.432323357440003,4.16874944146681));
#50325=CARTESIAN_POINT('Ctrl Pts',(12.7307170129634,0.398042271448426,4.23862566037754));
#50326=CARTESIAN_POINT('Ctrl Pts',(12.7385883850133,0.349231538304918,4.29617944234672));
#50327=CARTESIAN_POINT('Ctrl Pts',(12.7464597570633,0.300420805161409,4.35373322431589));
#50328=CARTESIAN_POINT('Ctrl Pts',(12.7543311291133,0.237080424865968,4.39896456934351));
#50329=CARTESIAN_POINT('Ctrl Pts',(12.7622025011632,0.166800374688878,4.42645347375649));
#50330=CARTESIAN_POINT('Ctrl Pts',(12.7681364312804,0.113818899065861,4.4471763206439));
#50331=CARTESIAN_POINT('Ctrl Pts',(12.7740703613976,0.056893551674301,4.45781599184163));
#50332=CARTESIAN_POINT('Ctrl Pts',(12.7800042915148,-1.13874042544416E-5,
4.45787212683272));
#50333=CARTESIAN_POINT('Origin',(12.5,0.,4.));
#50334=CARTESIAN_POINT('',(13.0800042915148,2.8196954984682E-6,4.45783894202495));
#50335=CARTESIAN_POINT('',(12.9699957084852,-6.90274666573233E-6,4.45790451736119));
#50336=CARTESIAN_POINT('',(12.5,-5.60735153159594E-17,4.457875));
#50337=CARTESIAN_POINT('Ctrl Pts',(12.9699957084852,-6.90274666573233E-6,
4.45790451736119));
#50338=CARTESIAN_POINT('Ctrl Pts',(12.9628865412726,0.0681543496286777,
4.45785453236543));
#50339=CARTESIAN_POINT('Ctrl Pts',(12.95577737406,0.136337475731944,4.44242789501186));
#50340=CARTESIAN_POINT('Ctrl Pts',(12.9486682068475,0.197807532932104,4.41298560914613));
#50341=CARTESIAN_POINT('Ctrl Pts',(12.9407968347975,0.265868063186489,4.38038668734267));
#50342=CARTESIAN_POINT('Ctrl Pts',(12.9329254627476,0.325698883531032,4.33060565060516));
#50343=CARTESIAN_POINT('Ctrl Pts',(12.9250540906976,0.370130557623211,4.26960768492436));
#50344=CARTESIAN_POINT('Ctrl Pts',(12.9171827186476,0.41456223171539,4.20860971924356));
#50345=CARTESIAN_POINT('Ctrl Pts',(12.9093113465977,0.443594759555206,4.13639482461947));
#50346=CARTESIAN_POINT('Ctrl Pts',(12.9014399745477,0.453749217534713,4.06161640217293));
#50347=CARTESIAN_POINT('Ctrl Pts',(12.8935686024978,0.463903675514219,3.9868379797264));
#50348=CARTESIAN_POINT('Ctrl Pts',(12.8856972304478,0.455180063633418,3.90949602945742));
#50349=CARTESIAN_POINT('Ctrl Pts',(12.8778258583979,0.428623718850503,3.83885831972366));
#50350=CARTESIAN_POINT('Ctrl Pts',(12.8699544863479,0.402067374067587,3.7682206099899));
#50351=CARTESIAN_POINT('Ctrl Pts',(12.862083114298,0.357678296382559,3.70428714079136));
#50352=CARTESIAN_POINT('Ctrl Pts',(12.854211742248,0.300775561959983,3.65471896268111));
#50353=CARTESIAN_POINT('Ctrl Pts',(12.846340370198,0.243872827537407,3.60515078457087));
#50354=CARTESIAN_POINT('Ctrl Pts',(12.8384689981481,0.174456436377283,3.56994789754891));
#50355=CARTESIAN_POINT('Ctrl Pts',(12.8305976260981,0.100844448250471,3.55332860992135));
#50356=CARTESIAN_POINT('Ctrl Pts',(12.8227262540482,0.0272324601236582,
3.53670932229378));
#50357=CARTESIAN_POINT('Ctrl Pts',(12.8148548819982,-0.0505751249698428,
3.53867363406062));
#50358=CARTESIAN_POINT('Ctrl Pts',(12.8069835099483,-0.123254740362562,
3.558986165072));
#50359=CARTESIAN_POINT('Ctrl Pts',(12.7991121378983,-0.195934355755281,
3.57929869608338));
#50360=CARTESIAN_POINT('Ctrl Pts',(12.7912407658484,-0.263486001447217,
3.6179594463393));
#50361=CARTESIAN_POINT('Ctrl Pts',(12.7833693937984,-0.317815070570116,
3.67033575613656));
#50362=CARTESIAN_POINT('Ctrl Pts',(12.7754980217484,-0.372144139693014,
3.72271206593382));
#50363=CARTESIAN_POINT('Ctrl Pts',(12.7676266496985,-0.413250632246875,
3.78880393527241));
#50364=CARTESIAN_POINT('Ctrl Pts',(12.7597552776485,-0.43620881068128,3.86069167744737));
#50365=CARTESIAN_POINT('Ctrl Pts',(12.7518839055986,-0.459166989115684,
3.93257941962233));
#50366=CARTESIAN_POINT('Ctrl Pts',(12.7440125335486,-0.463976853430633,
4.01026303463365));
#50367=CARTESIAN_POINT('Ctrl Pts',(12.7361411614987,-0.450062064178823,
4.08443380953254));
#50368=CARTESIAN_POINT('Ctrl Pts',(12.7282697894487,-0.436147274927012,
4.15860458443143));
#50369=CARTESIAN_POINT('Ctrl Pts',(12.7203984173988,-0.403507832108441,
4.22926251921788));
#50370=CARTESIAN_POINT('Ctrl Pts',(12.7125270453488,-0.356054829243877,
4.28794078818664));
#50371=CARTESIAN_POINT('Ctrl Pts',(12.7046556732988,-0.308601826379312,
4.3466190571554));
#50372=CARTESIAN_POINT('Ctrl Pts',(12.6967843012489,-0.246335263468753,
4.39331766030646));
#50373=CARTESIAN_POINT('Ctrl Pts',(12.6889129291989,-0.176716536654988,
4.42244075943884));
#50374=CARTESIAN_POINT('Ctrl Pts',(12.682607188961,-0.120945115332726,4.44577121528397));
#50375=CARTESIAN_POINT('Ctrl Pts',(12.6763014487231,-0.0604553842193124,
4.45782245132557));
#50376=CARTESIAN_POINT('Ctrl Pts',(12.6699957084852,1.09516003635735E-5,
4.45788309353564));
#50377=CARTESIAN_POINT('Ctrl Pts',(12.7800042915148,-1.13874042544416E-5,
4.45787212683272));
#50378=CARTESIAN_POINT('Ctrl Pts',(12.7819417334476,-0.0185909818676029,
4.45789045503738));
#50379=CARTESIAN_POINT('Ctrl Pts',(12.7838791753803,-0.0371684007279871,
4.45678053845584));
#50380=CARTESIAN_POINT('Ctrl Pts',(12.7858166173131,-0.0556056617636943,
4.45452496135198));
#50381=CARTESIAN_POINT('Ctrl Pts',(12.793687989363,-0.130511927980435,4.44536108073615));
#50382=CARTESIAN_POINT('Ctrl Pts',(12.801559361413,-0.203104740355178,4.41728685570614));
#50383=CARTESIAN_POINT('Ctrl Pts',(12.8094307334629,-0.264685413403174,
4.37366637792357));
#50384=CARTESIAN_POINT('Ctrl Pts',(12.8173021055129,-0.32626608645117,4.33004590014099));
#50385=CARTESIAN_POINT('Ctrl Pts',(12.8251734775629,-0.37683462017242,4.27087916960585));
#50386=CARTESIAN_POINT('Ctrl Pts',(12.8330448496128,-0.410331463567461,
4.20325604577686));
#50387=CARTESIAN_POINT('Ctrl Pts',(12.8409162216628,-0.443828306962503,
4.13563292194788));
#50388=CARTESIAN_POINT('Ctrl Pts',(12.8487875937127,-0.460253460031337,
4.05955340482505));
#50389=CARTESIAN_POINT('Ctrl Pts',(12.8566589657627,-0.457638721839564,
3.98413398734005));
#50390=CARTESIAN_POINT('Ctrl Pts',(12.8645303378126,-0.45502398364779,3.90871456985506));
#50391=CARTESIAN_POINT('Ctrl Pts',(12.8724017098626,-0.433369354195409,
3.8339552520079));
#50392=CARTESIAN_POINT('Ctrl Pts',(12.8802730819125,-0.395269674734573,
3.76881432927916));
#50393=CARTESIAN_POINT('Ctrl Pts',(12.8881444539625,-0.357169995273737,
3.70367340655041));
#50394=CARTESIAN_POINT('Ctrl Pts',(12.8960158260125,-0.302625265804445,
3.64815087894007));
#50395=CARTESIAN_POINT('Ctrl Pts',(12.9038871980624,-0.238171498431664,
3.6088999265713));
#50396=CARTESIAN_POINT('Ctrl Pts',(12.9117585701124,-0.173717731058884,
3.56964897420252));
#50397=CARTESIAN_POINT('Ctrl Pts',(12.9196299421623,-0.0993549257826154,
3.5466695970753));
#50398=CARTESIAN_POINT('Ctrl Pts',(12.9275013142123,-0.023993864556795,
3.54271537903906));
#50399=CARTESIAN_POINT('Ctrl Pts',(12.9353726862622,0.0513671966690251,
3.53876116100282));
#50400=CARTESIAN_POINT('Ctrl Pts',(12.9432440583122,0.127726513844396,3.55383210205756));
#50401=CARTESIAN_POINT('Ctrl Pts',(12.9511154303621,0.195934065997641,3.58612227423372));
#50402=CARTESIAN_POINT('Ctrl Pts',(12.9589868024121,0.264141618150887,3.61841244640988));
#50403=CARTESIAN_POINT('Ctrl Pts',(12.9668581744621,0.324197405282005,3.66792184970745));
#50404=CARTESIAN_POINT('Ctrl Pts',(12.974729546512,0.368905033668178,3.72871784755079));
#50405=CARTESIAN_POINT('Ctrl Pts',(12.982600918562,0.41361266205435,3.78951384539413));
#50406=CARTESIAN_POINT('Ctrl Pts',(12.9904722906119,0.442972131695578,3.86159643778324));
#50407=CARTESIAN_POINT('Ctrl Pts',(12.9983436626619,0.453465341949404,3.93632807718928));
#50408=CARTESIAN_POINT('Ctrl Pts',(13.0062150347118,0.46395855220323,4.01105971659532));
#50409=CARTESIAN_POINT('Ctrl Pts',(13.0140864067618,0.455585503069655,4.0884404030183));
#50410=CARTESIAN_POINT('Ctrl Pts',(13.0219577788117,0.429349524305901,4.15919772637108));
#50411=CARTESIAN_POINT('Ctrl Pts',(13.0298291508617,0.403113545542148,4.22995504972387));
#50412=CARTESIAN_POINT('Ctrl Pts',(13.0377005229117,0.359014637148215,4.29408901000646));
#50413=CARTESIAN_POINT('Ctrl Pts',(13.0455718949616,0.302337104315659,4.34391453219887));
#50414=CARTESIAN_POINT('Ctrl Pts',(13.0534432670116,0.245659571483104,4.39374005439127));
#50415=CARTESIAN_POINT('Ctrl Pts',(13.0613146390615,0.176403414211925,4.4292571384935));
#50416=CARTESIAN_POINT('Ctrl Pts',(13.0691860111115,0.102867492605122,4.44620982627979));
#50417=CARTESIAN_POINT('Ctrl Pts',(13.0727921045793,0.0691786509558273,
4.45397632191734));
#50418=CARTESIAN_POINT('Ctrl Pts',(13.076398198047,0.0345915681853763,4.45784650391406));
#50419=CARTESIAN_POINT('Ctrl Pts',(13.0800042915148,2.8196954984682E-6,
4.45783894202495));
#50420=CARTESIAN_POINT('Origin',(12.5,0.,4.));
#50421=CARTESIAN_POINT('',(13.3800042915148,1.00338821889499E-5,4.45789143379912));
#50422=CARTESIAN_POINT('',(13.2699957084852,-6.83105689078257E-6,4.45784477598907));
#50423=CARTESIAN_POINT('',(12.5,-5.60735153159594E-17,4.457875));
#50424=CARTESIAN_POINT('Ctrl Pts',(13.2699957084852,-6.83105689078257E-6,
4.45784477598907));
#50425=CARTESIAN_POINT('Ctrl Pts',(13.265214377922,0.0458528260712244,4.45782008288951));
#50426=CARTESIAN_POINT('Ctrl Pts',(13.2604330473589,0.091719698604501,4.45096974854549));
#50427=CARTESIAN_POINT('Ctrl Pts',(13.2556517167957,0.135506404234727,4.43740478719402));
#50428=CARTESIAN_POINT('Ctrl Pts',(13.2477803447458,0.207591244700251,4.41507316710824));
#50429=CARTESIAN_POINT('Ctrl Pts',(13.2399089726958,0.274038390871736,4.37454348113122));
#50430=CARTESIAN_POINT('Ctrl Pts',(13.2320376006459,0.326885582178656,4.32067233995558));
#50431=CARTESIAN_POINT('Ctrl Pts',(13.2241662285959,0.379732773485576,4.26680119877995));
#50432=CARTESIAN_POINT('Ctrl Pts',(13.2162948565459,0.418980009927931,4.19958860240569));
#50433=CARTESIAN_POINT('Ctrl Pts',(13.208423484496,0.439924354792367,4.12708853413817));
#50434=CARTESIAN_POINT('Ctrl Pts',(13.200552112446,0.460868699656804,4.05458846587065));
#50435=CARTESIAN_POINT('Ctrl Pts',(13.1926807403961,0.463510152943321,3.97680092570987));
#50436=CARTESIAN_POINT('Ctrl Pts',(13.1848093683461,0.447532193317848,3.90304707640827));
#50437=CARTESIAN_POINT('Ctrl Pts',(13.1769379962962,0.431554233692375,3.82929322710668));
#50438=CARTESIAN_POINT('Ctrl Pts',(13.1690666242462,0.396956861154912,3.75957306866428));
#50439=CARTESIAN_POINT('Ctrl Pts',(13.1611952521963,0.347885826291745,3.70224106173923));
#50440=CARTESIAN_POINT('Ctrl Pts',(13.1533238801463,0.298814791428577,3.64490905481418));
#50441=CARTESIAN_POINT('Ctrl Pts',(13.1454525080963,0.235270094239705,3.59996519940648));
#50442=CARTESIAN_POINT('Ctrl Pts',(13.1375811360464,0.164866199243897,3.57279504942506));
#50443=CARTESIAN_POINT('Ctrl Pts',(13.1297097639964,0.0944623042480882,
3.54562489944363));
#50444=CARTESIAN_POINT('Ctrl Pts',(13.1218383919465,0.0171992114453437,
3.53622845488849));
#50445=CARTESIAN_POINT('Ctrl Pts',(13.1139670198965,-0.0576647601420857,
3.54573167743434));
#50446=CARTESIAN_POINT('Ctrl Pts',(13.1060956478466,-0.132528731729515,
3.55523489998019));
#50447=CARTESIAN_POINT('Ctrl Pts',(13.0982242757966,-0.204993582101629,
3.58363778962703));
#50448=CARTESIAN_POINT('Ctrl Pts',(13.0903529037467,-0.266375958336211,
3.62753687126191));
#50449=CARTESIAN_POINT('Ctrl Pts',(13.0824815316967,-0.327758334570793,
3.67143595289679));
#50450=CARTESIAN_POINT('Ctrl Pts',(13.0746101596467,-0.378058236667844,
3.73083122651971));
#50451=CARTESIAN_POINT('Ctrl Pts',(13.0667387875968,-0.411248303781717,
3.79860544673343));
#50452=CARTESIAN_POINT('Ctrl Pts',(13.0588674155468,-0.444438370895591,
3.86637966694714));
#50453=CARTESIAN_POINT('Ctrl Pts',(13.0509960434969,-0.460518603026287,
3.94253283375165));
#50454=CARTESIAN_POINT('Ctrl Pts',(13.0431246714469,-0.457562130387816,
4.0179396288708));
#50455=CARTESIAN_POINT('Ctrl Pts',(13.035253299397,-0.454605657749345,4.09334642398995));
#50456=CARTESIAN_POINT('Ctrl Pts',(13.027381927347,-0.432612480341706,4.16800684742375));
#50457=CARTESIAN_POINT('Ctrl Pts',(13.0195105552971,-0.394218007200806,
4.23297445406563));
#50458=CARTESIAN_POINT('Ctrl Pts',(13.0116391832471,-0.355823534059905,
4.29794206070751));
#50459=CARTESIAN_POINT('Ctrl Pts',(13.0037678111972,-0.301027765185743,
4.35321685055749));
#50460=CARTESIAN_POINT('Ctrl Pts',(12.9958964391472,-0.236396794305188,
4.39217532952931));
#50461=CARTESIAN_POINT('Ctrl Pts',(12.9880250670972,-0.171765823424632,
4.43113380850113));
#50462=CARTESIAN_POINT('Ctrl Pts',(12.9801536950473,-0.0972996505376846,
4.45377597659478));
#50463=CARTESIAN_POINT('Ctrl Pts',(12.9722823229973,-0.0219214440120968,
4.4573886572069));
#50464=CARTESIAN_POINT('Ctrl Pts',(12.9715201181599,-0.014622381881285,
4.45773848219561));
#50465=CARTESIAN_POINT('Ctrl Pts',(12.9707579133226,-0.00731476803234869,
4.45790987647069));
#50466=CARTESIAN_POINT('Ctrl Pts',(12.9699957084852,-6.90274666573233E-6,
4.45790451736119));
#50467=CARTESIAN_POINT('Ctrl Pts',(13.0800042915148,2.8196954984682E-6,
4.45783894202495));
#50468=CARTESIAN_POINT('Ctrl Pts',(13.084269570097,-0.0409086678841046,
4.4578299978409));
#50469=CARTESIAN_POINT('Ctrl Pts',(13.0885348486792,-0.0818224858219862,
4.45239605085009));
#50470=CARTESIAN_POINT('Ctrl Pts',(13.0928001272613,-0.121255029803553,
4.44156782927524));
#50471=CARTESIAN_POINT('Ctrl Pts',(13.1006714993113,-0.194025944662995,
4.42158485301405));
#50472=CARTESIAN_POINT('Ctrl Pts',(13.1085428713613,-0.261752088439453,
4.3832306090213));
#50473=CARTESIAN_POINT('Ctrl Pts',(13.1164142434112,-0.31631794022257,4.33110102808186));
#50474=CARTESIAN_POINT('Ctrl Pts',(13.1242856154612,-0.370883792005687,
4.27897144714243));
#50475=CARTESIAN_POINT('Ctrl Pts',(13.1321569875111,-0.412289351795463,
4.21306652925631));
#50476=CARTESIAN_POINT('Ctrl Pts',(13.1400283595611,-0.435573054271055,
4.14128356060242));
#50477=CARTESIAN_POINT('Ctrl Pts',(13.147899731611,-0.458856756746647,4.06950059194853));
#50478=CARTESIAN_POINT('Ctrl Pts',(13.155771103661,-0.464018601908056,3.99183957252686));
#50479=CARTESIAN_POINT('Ctrl Pts',(13.1636424757109,-0.45044005369213,3.91760650430194));
#50480=CARTESIAN_POINT('Ctrl Pts',(13.1715138477609,-0.436861505476204,
3.84337343607703));
#50481=CARTESIAN_POINT('Ctrl Pts',(13.1793852198109,-0.404542563882944,
3.77256831904885));
#50482=CARTESIAN_POINT('Ctrl Pts',(13.1872565918608,-0.357355958580309,
3.7136756228145));
#50483=CARTESIAN_POINT('Ctrl Pts',(13.1951279639108,-0.310169353277673,
3.65478292658016));
#50484=CARTESIAN_POINT('Ctrl Pts',(13.2029993359607,-0.248115084265664,
3.60780265113964));
#50485=CARTESIAN_POINT('Ctrl Pts',(13.2108707080107,-0.178629020319019,
3.57836437152041));
#50486=CARTESIAN_POINT('Ctrl Pts',(13.2187420800606,-0.109142956372374,
3.54892609190117));
#50487=CARTESIAN_POINT('Ctrl Pts',(13.2266134521106,-0.0322250974910928,
3.53702980810322));
#50488=CARTESIAN_POINT('Ctrl Pts',(13.2344848241605,0.0429076061587562,
3.54410103373967));
#50489=CARTESIAN_POINT('Ctrl Pts',(13.2423561962105,0.118040309808605,3.55117225937612));
#50490=CARTESIAN_POINT('Ctrl Pts',(13.2502275682605,0.191387858227023,3.57721099444696));
#50491=CARTESIAN_POINT('Ctrl Pts',(13.2580989403104,0.254161126126225,3.61909705689013));
#50492=CARTESIAN_POINT('Ctrl Pts',(13.2659703123604,0.316934394025428,3.66098311933329));
#50493=CARTESIAN_POINT('Ctrl Pts',(13.2738416844103,0.369133381405416,3.71871650914877));
#50494=CARTESIAN_POINT('Ctrl Pts',(13.2817130564603,0.404503162915977,3.78537912195109));
#50495=CARTESIAN_POINT('Ctrl Pts',(13.2895844285102,0.43987294442654,3.85204173475342));
#50496=CARTESIAN_POINT('Ctrl Pts',(13.2974558005602,0.458413520067676,3.92763357054259));
#50497=CARTESIAN_POINT('Ctrl Pts',(13.3053271726101,0.457903200829578,4.00309657448501));
#50498=CARTESIAN_POINT('Ctrl Pts',(13.3131985446601,0.457392881591479,4.07855957842742));
#50499=CARTESIAN_POINT('Ctrl Pts',(13.3210699167101,0.437831667474148,4.15389375052308));
#50500=CARTESIAN_POINT('Ctrl Pts',(13.32894128876,0.401563549045306,4.22007191138728));
#50501=CARTESIAN_POINT('Ctrl Pts',(13.33681266081,0.365295430616463,4.28625007225149));
#50502=CARTESIAN_POINT('Ctrl Pts',(13.3446840328599,0.31232040787611,4.34327222188425));
#50503=CARTESIAN_POINT('Ctrl Pts',(13.3525554049099,0.248986397312635,4.38430548273058));
#50504=CARTESIAN_POINT('Ctrl Pts',(13.3604267769598,0.185652386749161,4.42533874357692));
#50505=CARTESIAN_POINT('Ctrl Pts',(13.3682981490098,0.111959388362564,4.45038311563682));
#50506=CARTESIAN_POINT('Ctrl Pts',(13.3761695210597,0.0367379221854645,
4.45643756985705));
#50507=CARTESIAN_POINT('Ctrl Pts',(13.3774477778781,0.024522472144774,4.45742077168506));
#50508=CARTESIAN_POINT('Ctrl Pts',(13.3787260346965,0.0122667140672706,
4.45790318029249));
#50509=CARTESIAN_POINT('Ctrl Pts',(13.3800042915148,1.00338821889499E-5,
4.45789143379912));
#50510=CARTESIAN_POINT('Origin',(12.5,0.,4.));
#50511=CARTESIAN_POINT('',(13.6800042915148,-8.85210990424201E-6,4.45789764648838));
#50512=CARTESIAN_POINT('',(13.5699957084852,1.03170790782398E-5,4.4578580083501));
#50513=CARTESIAN_POINT('',(12.5,-5.60735153159594E-17,4.457875));
#50514=CARTESIAN_POINT('Ctrl Pts',(13.5699957084852,1.03170790782398E-5,
4.4578580083501));
#50515=CARTESIAN_POINT('Ctrl Pts',(13.5675422145714,0.0235408097699949,
4.45787795556699));
#50516=CARTESIAN_POINT('Ctrl Pts',(13.5650887206577,0.0470683081483061,
4.45609516914004));
#50517=CARTESIAN_POINT('Ctrl Pts',(13.562635226744,0.0703115975725277,4.45248338388903));
#50518=CARTESIAN_POINT('Ctrl Pts',(13.554763854694,0.144881409096958,4.44089594716616));
#50519=CARTESIAN_POINT('Ctrl Pts',(13.5468924826441,0.21652593236894,4.41048310506186));
#50520=CARTESIAN_POINT('Ctrl Pts',(13.5390211105941,0.276660113016528,4.36488918223832));
#50521=CARTESIAN_POINT('Ctrl Pts',(13.5311497385442,0.336794293664116,4.31929525941478));
#50522=CARTESIAN_POINT('Ctrl Pts',(13.5232783664942,0.385418131687311,4.25852025587201));
#50523=CARTESIAN_POINT('Ctrl Pts',(13.5154069944443,0.416705106451492,4.18984674794718));
#50524=CARTESIAN_POINT('Ctrl Pts',(13.5075356223943,0.447992081215673,4.12117324002235));
#50525=CARTESIAN_POINT('Ctrl Pts',(13.4996642503443,0.461942192720839,4.04460122771548));
#50526=CARTESIAN_POINT('Ctrl Pts',(13.4917928782944,0.456883820300162,3.96930621892307));
#50527=CARTESIAN_POINT('Ctrl Pts',(13.4839215062444,0.451825447879485,3.89401121013066));
#50528=CARTESIAN_POINT('Ctrl Pts',(13.4760501341945,0.427758591532965,3.81999320485271));
#50529=CARTESIAN_POINT('Ctrl Pts',(13.4681787621445,0.387567146091087,3.75612166820384));
#50530=CARTESIAN_POINT('Ctrl Pts',(13.4603073900946,0.347375700649209,3.69225013155497));
#50531=CARTESIAN_POINT('Ctrl Pts',(13.4524360180446,0.291059666111973,3.63852506353517));
#50532=CARTESIAN_POINT('Ctrl Pts',(13.4445646459947,0.225367307335285,3.60138425741911));
#50533=CARTESIAN_POINT('Ctrl Pts',(13.4366932739447,0.159674948558598,3.56424345130305));
#50534=CARTESIAN_POINT('Ctrl Pts',(13.4288219018947,0.0846062655424597,
3.54368690709073));
#50535=CARTESIAN_POINT('Ctrl Pts',(13.4209505298448,0.00915662451852634,
3.54217788424291));
#50536=CARTESIAN_POINT('Ctrl Pts',(13.4130791577948,-0.0662930165054059,
3.54066886139509));
#50537=CARTESIAN_POINT('Ctrl Pts',(13.4052077857449,-0.142123615537132,
3.55820735991178));
#50538=CARTESIAN_POINT('Ctrl Pts',(13.3973364136949,-0.209248507106454,
3.5926917681625));
#50539=CARTESIAN_POINT('Ctrl Pts',(13.389465041645,-0.276373398675776,3.62717617641322));
#50540=CARTESIAN_POINT('Ctrl Pts',(13.381593669595,-0.334792582782693,3.67860649439798));
#50541=CARTESIAN_POINT('Ctrl Pts',(13.3737222975451,-0.377505777353741,
3.74081990525232));
#50542=CARTESIAN_POINT('Ctrl Pts',(13.3658509254951,-0.420218971924789,
3.80303331610666));
#50543=CARTESIAN_POINT('Ctrl Pts',(13.3579795534451,-0.44722617695997,3.87602981983059));
#50544=CARTESIAN_POINT('Ctrl Pts',(13.3501081813952,-0.455291160112798,
3.95106235628872));
#50545=CARTESIAN_POINT('Ctrl Pts',(13.3422368093452,-0.463356143265626,
4.02609489274685));
#50546=CARTESIAN_POINT('Ctrl Pts',(13.3343654372953,-0.452478904536101,
4.10316346193917));
#50547=CARTESIAN_POINT('Ctrl Pts',(13.3264940652453,-0.423962846915058,
4.17303305431203));
#50548=CARTESIAN_POINT('Ctrl Pts',(13.3186226931954,-0.395446789294015,
4.24290264668488));
#50549=CARTESIAN_POINT('Ctrl Pts',(13.3107513211454,-0.349291912781453,
4.30557326223827));
#50550=CARTESIAN_POINT('Ctrl Pts',(13.3028799490955,-0.291028886105345,
4.35353517632783));
#50551=CARTESIAN_POINT('Ctrl Pts',(13.2950085770455,-0.232765859429236,
4.4014970904174));
#50552=CARTESIAN_POINT('Ctrl Pts',(13.2871372049956,-0.162394682589579,
4.43475030304313));
#50553=CARTESIAN_POINT('Ctrl Pts',(13.2792658329456,-0.0883478267899694,
4.44931013225873));
#50554=CARTESIAN_POINT('Ctrl Pts',(13.2761757914588,-0.059279469337623,
4.4550258417985));
#50555=CARTESIAN_POINT('Ctrl Pts',(13.273085749972,-0.0296446570187532,
4.45786073445524));
#50556=CARTESIAN_POINT('Ctrl Pts',(13.2699957084852,-6.83105689078257E-6,
4.45784477598907));
#50557=CARTESIAN_POINT('Ctrl Pts',(13.3800042915148,1.00338821889499E-5,
4.45789143379912));
#50558=CARTESIAN_POINT('Ctrl Pts',(13.3865974067464,-0.0632086430349686,
4.45783084661254));
#50559=CARTESIAN_POINT('Ctrl Pts',(13.393190521978,-0.12645185159805,4.44462381290384));
#50560=CARTESIAN_POINT('Ctrl Pts',(13.3997836372096,-0.184315051738561,
4.41918121595096));
#50561=CARTESIAN_POINT('Ctrl Pts',(13.4076550092596,-0.253396625517876,
4.3888058714441));
#50562=CARTESIAN_POINT('Ctrl Pts',(13.4155263813095,-0.314809839108902,
4.34099064604983));
#50563=CARTESIAN_POINT('Ctrl Pts',(13.4233977533595,-0.361195640434018,
4.28146516557999));
#50564=CARTESIAN_POINT('Ctrl Pts',(13.4312691254094,-0.407581441759134,
4.22193968511016));
#50565=CARTESIAN_POINT('Ctrl Pts',(13.4391404974594,-0.438939830818339,
4.15070394956476));
#50566=CARTESIAN_POINT('Ctrl Pts',(13.4470118695093,-0.451513179494438,
4.07629402890356));
#50567=CARTESIAN_POINT('Ctrl Pts',(13.4548832415593,-0.464086528170537,
4.00188410824235));
#50568=CARTESIAN_POINT('Ctrl Pts',(13.4627546136093,-0.457874836463529,
3.92430000246534));
#50569=CARTESIAN_POINT('Ctrl Pts',(13.4706259856592,-0.433622441953051,
3.85283849709185));
#50570=CARTESIAN_POINT('Ctrl Pts',(13.4784973577092,-0.409370047442573,
3.78137699171835));
#50571=CARTESIAN_POINT('Ctrl Pts',(13.4863687297591,-0.367076950128625,
3.71603808674838));
#50572=CARTESIAN_POINT('Ctrl Pts',(13.4942401018091,-0.311811067605128,
3.66465124389307));
#50573=CARTESIAN_POINT('Ctrl Pts',(13.502111473859,-0.25654518508163,3.61326440103776));
#50574=CARTESIAN_POINT('Ctrl Pts',(13.509982845909,-0.188306517348584,3.5758296202971));
#50575=CARTESIAN_POINT('Ctrl Pts',(13.5178542179589,-0.115272000283325,
3.55683265457144));
#50576=CARTESIAN_POINT('Ctrl Pts',(13.5257255900089,-0.0422374832180674,
3.53783568884578));
#50577=CARTESIAN_POINT('Ctrl Pts',(13.5335969620589,0.035592883179403,3.53727653813511));
#50578=CARTESIAN_POINT('Ctrl Pts',(13.5414683341088,0.108892804353757,3.55522220461956));
#50579=CARTESIAN_POINT('Ctrl Pts',(13.5493397061588,0.182192725528112,3.573167871104));
#50580=CARTESIAN_POINT('Ctrl Pts',(13.5572110782087,0.250962201479351,3.60961835478357));
#50581=CARTESIAN_POINT('Ctrl Pts',(13.5650824502587,0.306960690387823,3.66020584957927));
#50582=CARTESIAN_POINT('Ctrl Pts',(13.5729538223086,0.362959179296295,3.71079334437498));
#50583=CARTESIAN_POINT('Ctrl Pts',(13.5808251943586,0.406186681162,3.77551785028682));
#50584=CARTESIAN_POINT('Ctrl Pts',(13.5886965664085,0.431463310113251,3.84662352810933));
#50585=CARTESIAN_POINT('Ctrl Pts',(13.5965679384585,0.456739939064502,3.91772920593184));
#50586=CARTESIAN_POINT('Ctrl Pts',(13.6044393105085,0.464065695101298,3.99521605566501));
#50587=CARTESIAN_POINT('Ctrl Pts',(13.6123106825584,0.452562744007997,4.06979894583348));
#50588=CARTESIAN_POINT('Ctrl Pts',(13.6201820546084,0.441059792914696,4.14438183600196));
#50589=CARTESIAN_POINT('Ctrl Pts',(13.6280534266583,0.410728134691299,4.21606076660573));
#50590=CARTESIAN_POINT('Ctrl Pts',(13.6359247987083,0.365202365858889,4.27624656029457));
#50591=CARTESIAN_POINT('Ctrl Pts',(13.6437961707582,0.319676597026479,4.33643235398341));
#50592=CARTESIAN_POINT('Ctrl Pts',(13.6516675428082,0.258956717585058,4.38512501075732));
#50593=CARTESIAN_POINT('Ctrl Pts',(13.6595389148581,0.190318698434502,4.41648976353532));
#50594=CARTESIAN_POINT('Ctrl Pts',(13.666360707077,0.130832969391341,4.44367229602021));
#50595=CARTESIAN_POINT('Ctrl Pts',(13.6731824992959,0.065399948454096,4.45783988979956));
#50596=CARTESIAN_POINT('Ctrl Pts',(13.6800042915148,-8.85210990424201E-6,
4.45789764648838));
#50597=CARTESIAN_POINT('Origin',(12.5,0.,4.));
#50598=CARTESIAN_POINT('',(13.9800042915148,-4.68615130337092E-6,4.45784092071359));
#50599=CARTESIAN_POINT('',(13.8699957084852,1.23414887176878E-6,4.4579133809027));
#50600=CARTESIAN_POINT('',(12.5,-5.60735153159594E-17,4.457875));
#50601=CARTESIAN_POINT('Ctrl Pts',(13.8699957084852,1.23414887176878E-6,
4.4579133809027));
#50602=CARTESIAN_POINT('Ctrl Pts',(13.8698700512209,0.00120594270822336,
4.45791357044259));
#50603=CARTESIAN_POINT('Ctrl Pts',(13.8697443939566,0.00241064979645091,
4.45790891401425));
#50604=CARTESIAN_POINT('Ctrl Pts',(13.8696187366923,0.00361531855258033,
4.45789940262096));
#50605=CARTESIAN_POINT('Ctrl Pts',(13.8617473646423,0.0790776965455978,
4.45730359373015));
#50606=CARTESIAN_POINT('Ctrl Pts',(13.8538759925924,0.154389660535011,4.43765704798318));
#50607=CARTESIAN_POINT('Ctrl Pts',(13.8460046205424,0.22052669229976,4.40131398110731));
#50608=CARTESIAN_POINT('Ctrl Pts',(13.8381332484924,0.286663724064511,4.36497091423144));
#50609=CARTESIAN_POINT('Ctrl Pts',(13.8302618764425,0.343625823604597,4.31193132622667));
#50610=CARTESIAN_POINT('Ctrl Pts',(13.8223905043925,0.384587309076409,4.24855087033892));
#50611=CARTESIAN_POINT('Ctrl Pts',(13.8145191323426,0.42554879454822,4.18517041445118));
#50612=CARTESIAN_POINT('Ctrl Pts',(13.8066477602926,0.450509665951756,4.11144909068046));
#50613=CARTESIAN_POINT('Ctrl Pts',(13.7987763882427,0.456478899990553,4.03622081324714));
#50614=CARTESIAN_POINT('Ctrl Pts',(13.7909050161927,0.46244813402935,3.96099253581381));
#50615=CARTESIAN_POINT('Ctrl Pts',(13.7830336441427,0.449425730703409,3.88425730471787));
#50616=CARTESIAN_POINT('Ctrl Pts',(13.7751622720928,0.418972144817937,3.81521018611534));
#50617=CARTESIAN_POINT('Ctrl Pts',(13.7672909000428,0.388518558932466,3.74616306751281));
#50618=CARTESIAN_POINT('Ctrl Pts',(13.7594195279929,0.340633790487464,3.68480406140369));
#50619=CARTESIAN_POINT('Ctrl Pts',(13.7515481559429,0.281055798532888,3.6384857242654));
#50620=CARTESIAN_POINT('Ctrl Pts',(13.743676783893,0.221477806578313,3.59216738712712));
#50621=CARTESIAN_POINT('Ctrl Pts',(13.735805411843,0.150206591114165,3.56088971895966));
#50622=CARTESIAN_POINT('Ctrl Pts',(13.7279340397931,0.0757824736049535,
3.54840067521841));
#50623=CARTESIAN_POINT('Ctrl Pts',(13.7200626677431,0.00135835609574232,
3.53591163147717));
#50624=CARTESIAN_POINT('Ctrl Pts',(13.7121912956931,-0.0762186634585312,
3.54221121216214));
#50625=CARTESIAN_POINT('Ctrl Pts',(13.7043199236432,-0.14765264866984,3.56654454809098));
#50626=CARTESIAN_POINT('Ctrl Pts',(13.6964485515932,-0.219086633881149,
3.59087788401983));
#50627=CARTESIAN_POINT('Ctrl Pts',(13.6885771795433,-0.284377584749494,
3.63324497519255));
#50628=CARTESIAN_POINT('Ctrl Pts',(13.6807058074933,-0.335701785830877,
3.68856903744356));
#50629=CARTESIAN_POINT('Ctrl Pts',(13.6728344354434,-0.38702598691226,3.74389309969457));
#50630=CARTESIAN_POINT('Ctrl Pts',(13.6649630633934,-0.424383438206683,
3.81217413302386));
#50631=CARTESIAN_POINT('Ctrl Pts',(13.6570916913435,-0.443297653083863,
3.88523012494906));
#50632=CARTESIAN_POINT('Ctrl Pts',(13.6492203192935,-0.462211867961044,
3.95828611687427));
#50633=CARTESIAN_POINT('Ctrl Pts',(13.6413489472436,-0.462682846420982,
4.03611706739538));
#50634=CARTESIAN_POINT('Ctrl Pts',(13.6334775751936,-0.444654151830396,
4.10939661196244));
#50635=CARTESIAN_POINT('Ctrl Pts',(13.6256062031436,-0.42662545723981,4.18267615652949));
#50636=CARTESIAN_POINT('Ctrl Pts',(13.6177348310937,-0.3900970895987,4.25140429514248));
#50637=CARTESIAN_POINT('Ctrl Pts',(13.6098634590437,-0.339446187702822,
4.3073454393722));
#50638=CARTESIAN_POINT('Ctrl Pts',(13.6019920869938,-0.288795285806945,
4.36328658360191));
#50639=CARTESIAN_POINT('Ctrl Pts',(13.5941207149438,-0.224021849656302,
4.40644073344835));
#50640=CARTESIAN_POINT('Ctrl Pts',(13.5862493428939,-0.152887581692542,
4.43163679270085));
#50641=CARTESIAN_POINT('Ctrl Pts',(13.5808314647576,-0.103925749791867,
4.44897928111035));
#50642=CARTESIAN_POINT('Ctrl Pts',(13.5754135866214,-0.0519504158054226,
4.45781396031326));
#50643=CARTESIAN_POINT('Ctrl Pts',(13.5699957084852,1.03170790782398E-5,
4.4578580083501));
#50644=CARTESIAN_POINT('Ctrl Pts',(13.6800042915148,-8.85210990424201E-6,
4.45789764648838));
#50645=CARTESIAN_POINT('Ctrl Pts',(13.6810538713459,-0.010072447664127,
4.45790653275371));
#50646=CARTESIAN_POINT('Ctrl Pts',(13.6821034511769,-0.0201354698749596,
4.45758141170421));
#50647=CARTESIAN_POINT('Ctrl Pts',(13.683153031008,-0.0301761699425476,
4.45691829561871));
#50648=CARTESIAN_POINT('Ctrl Pts',(13.691024403058,-0.105476860309351,4.45194522614199));
#50649=CARTESIAN_POINT('Ctrl Pts',(13.6988957751079,-0.179522082183268,
4.42796223840642));
#50650=CARTESIAN_POINT('Ctrl Pts',(13.7067671471579,-0.24343910912634,4.38784317739428));
#50651=CARTESIAN_POINT('Ctrl Pts',(13.7146385192078,-0.307356136069411,
4.34772411638213));
#50652=CARTESIAN_POINT('Ctrl Pts',(13.7225098912578,-0.361144968081636,
4.2914689820934));
#50653=CARTESIAN_POINT('Ctrl Pts',(13.7303812633077,-0.398360171146024,
4.22581874179975));
#50654=CARTESIAN_POINT('Ctrl Pts',(13.7382526353577,-0.435575374210412,
4.1601685015061));
#50655=CARTESIAN_POINT('Ctrl Pts',(13.7461240074077,-0.456216948326962,
4.08512315520753));
#50656=CARTESIAN_POINT('Ctrl Pts',(13.7539953794576,-0.457811445030669,
4.00967527273228));
#50657=CARTESIAN_POINT('Ctrl Pts',(13.7618667515076,-0.459405941734377,
3.93422739025703));
#50658=CARTESIAN_POINT('Ctrl Pts',(13.7697381235575,-0.441953361025241,
3.85837697160509));
#50659=CARTESIAN_POINT('Ctrl Pts',(13.7776094956075,-0.407545019133394,
3.79121305720166));
#50660=CARTESIAN_POINT('Ctrl Pts',(13.7854808676574,-0.373136677241547,
3.72404914279823));
#50661=CARTESIAN_POINT('Ctrl Pts',(13.7933522397074,-0.321772574166988,
3.6655717326433));
#50662=CARTESIAN_POINT('Ctrl Pts',(13.8012236117573,-0.259607592342073,
3.6227880859492));
#50663=CARTESIAN_POINT('Ctrl Pts',(13.8090949838073,-0.19744261051716,3.5800044392551));
#50664=CARTESIAN_POINT('Ctrl Pts',(13.8169663558573,-0.124476749941891,
3.55291455602183));
#50665=CARTESIAN_POINT('Ctrl Pts',(13.8248377279072,-0.0494533988297167,
3.54476457579874));
#50666=CARTESIAN_POINT('Ctrl Pts',(13.8327090999572,0.0255699522824598,
3.53661459557564));
#50667=CARTESIAN_POINT('Ctrl Pts',(13.8405804720071,0.102650793931542,3.54740451836272));
#50668=CARTESIAN_POINT('Ctrl Pts',(13.8484518440571,0.172552645974024,3.57584140410587));
#50669=CARTESIAN_POINT('Ctrl Pts',(13.856323216107,0.242454498016503,3.60427828984902));
#50670=CARTESIAN_POINT('Ctrl Pts',(13.864194588157,0.305177360452382,3.65036213854823));
#50671=CARTESIAN_POINT('Ctrl Pts',(13.8720659602069,0.353205247972751,3.70857079263049));
#50672=CARTESIAN_POINT('Ctrl Pts',(13.8799373322569,0.40123313549312,3.76677944671275));
#50673=CARTESIAN_POINT('Ctrl Pts',(13.8878087043068,0.434566048097978,3.83711290617806));
#50674=CARTESIAN_POINT('Ctrl Pts',(13.8956800763568,0.44920975351361,3.9111432194385));
#50675=CARTESIAN_POINT('Ctrl Pts',(13.9035514484068,0.463853458929242,3.98517353269893));
#50676=CARTESIAN_POINT('Ctrl Pts',(13.9114228204567,0.459807957155645,4.06290069975448));
#50677=CARTESIAN_POINT('Ctrl Pts',(13.9192941925067,0.437558014523894,4.13501079227018));
#50678=CARTESIAN_POINT('Ctrl Pts',(13.9271655645566,0.415308071892144,4.20712088478587));
#50679=CARTESIAN_POINT('Ctrl Pts',(13.9350369366066,0.374853688402242,4.27361390276169));
#50680=CARTESIAN_POINT('Ctrl Pts',(13.9429083086565,0.321042451364188,4.32652208887851));
#50681=CARTESIAN_POINT('Ctrl Pts',(13.9507796807065,0.267231214326134,4.37943027499533));
#50682=CARTESIAN_POINT('Ctrl Pts',(13.9586510527564,0.200063123739928,4.41875362925314));
#50683=CARTESIAN_POINT('Ctrl Pts',(13.9665224248064,0.127586829849962,4.43978009385641));
#50684=CARTESIAN_POINT('Ctrl Pts',(13.9710163803759,0.086208370984788,4.45178460807712));
#50685=CARTESIAN_POINT('Ctrl Pts',(13.9755103359454,0.0430996806131821,
4.45782517307841));
#50686=CARTESIAN_POINT('Ctrl Pts',(13.9800042915148,-4.68615130337092E-6,
4.45784092071359));
#50687=CARTESIAN_POINT('Origin',(12.5,0.,4.));
#50688=CARTESIAN_POINT('',(14.2800042915148,1.11332528513013E-5,4.45786561359635));
#50689=CARTESIAN_POINT('',(14.1699957084852,-1.10604184835328E-5,4.4578646218584));
#50690=CARTESIAN_POINT('',(12.5,-5.60735153159594E-17,4.457875));
#50691=CARTESIAN_POINT('Ctrl Pts',(14.1699957084852,-1.10604184835328E-5,
4.4578646218584));
#50692=CARTESIAN_POINT('Ctrl Pts',(14.1643265158203,0.0543576752587709,
4.45781404039958));
#50693=CARTESIAN_POINT('Ctrl Pts',(14.1586573231555,0.108743966382031,4.44812254260427));
#50694=CARTESIAN_POINT('Ctrl Pts',(14.1529881304907,0.159684023833442,4.42916890146099));
#50695=CARTESIAN_POINT('Ctrl Pts',(14.1451167584407,0.230411580321883,4.40285278028461));
#50696=CARTESIAN_POINT('Ctrl Pts',(14.1372453863907,0.294495541512382,4.358681244225));
#50697=CARTESIAN_POINT('Ctrl Pts',(14.1293740143408,0.344256823700223,4.30194730133701));
#50698=CARTESIAN_POINT('Ctrl Pts',(14.1215026422908,0.394018105888063,4.24521335844902));
#50699=CARTESIAN_POINT('Ctrl Pts',(14.1136312702409,0.429456709073245,4.17591700873265));
#50700=CARTESIAN_POINT('Ctrl Pts',(14.1057598981909,0.446326079279053,4.10236192849032));
#50701=CARTESIAN_POINT('Ctrl Pts',(14.097888526141,0.46319544948486,4.02880684824799));
#50702=CARTESIAN_POINT('Ctrl Pts',(14.090017154091,0.461495586711293,3.95099303747972));
#50703=CARTESIAN_POINT('Ctrl Pts',(14.0821457820411,0.441430182931853,3.87824480690492));
#50704=CARTESIAN_POINT('Ctrl Pts',(14.0742744099911,0.421364779152413,3.80549657633012));
#50705=CARTESIAN_POINT('Ctrl Pts',(14.0664030379411,0.3829338343671,3.73781392594881));
#50706=CARTESIAN_POINT('Ctrl Pts',(14.0585316658912,0.330742470300218,3.68330716492384));
#50707=CARTESIAN_POINT('Ctrl Pts',(14.0506602938412,0.278551106233337,3.62880040389886));
#50708=CARTESIAN_POINT('Ctrl Pts',(14.0427889217913,0.212599322884887,3.58746953223022));
#50709=CARTESIAN_POINT('Ctrl Pts',(14.0349175497413,0.140790022250932,3.5642671654747));
#50710=CARTESIAN_POINT('Ctrl Pts',(14.0270461776914,0.0689807216169763,
3.54106479871918));
#50711=CARTESIAN_POINT('Ctrl Pts',(14.0191748056414,-0.00868609630248519,
3.53599093687678));
#50712=CARTESIAN_POINT('Ctrl Pts',(14.0113034335915,-0.0829037347177578,
3.5496535731032));
#50713=CARTESIAN_POINT('Ctrl Pts',(14.0034320615415,-0.15712137313303,3.56331620932962));
#50714=CARTESIAN_POINT('Ctrl Pts',(13.9955606894916,-0.227889832044114,
3.59571534362485));
#50715=CARTESIAN_POINT('Ctrl Pts',(13.9876893174416,-0.286729034540398,
3.64296863695132));
#50716=CARTESIAN_POINT('Ctrl Pts',(13.9798179453916,-0.345568237036683,
3.69022193027778));
#50717=CARTESIAN_POINT('Ctrl Pts',(13.9719465733417,-0.392478183118168,
3.75232938263547));
#50718=CARTESIAN_POINT('Ctrl Pts',(13.9640752012917,-0.421837725217638,
3.82184875237013));
#50719=CARTESIAN_POINT('Ctrl Pts',(13.9562038292418,-0.451197267317109,
3.8913681221048));
#50720=CARTESIAN_POINT('Ctrl Pts',(13.9483324571918,-0.463006405434566,
3.96829940921644));
#50721=CARTESIAN_POINT('Ctrl Pts',(13.9404610851419,-0.455850068491383,
4.04342405445454));
#50722=CARTESIAN_POINT('Ctrl Pts',(13.9325897130919,-0.448693731548199,
4.11854869969265));
#50723=CARTESIAN_POINT('Ctrl Pts',(13.924718341042,-0.422571919544373,4.19186670305722));
#50724=CARTESIAN_POINT('Ctrl Pts',(13.916846968992,-0.38061476952465,4.25459247959939));
#50725=CARTESIAN_POINT('Ctrl Pts',(13.908975596942,-0.338657619504927,4.31731825614156));
#50726=CARTESIAN_POINT('Ctrl Pts',(13.9011042248921,-0.280865131469307,
4.36945180586132));
#50727=CARTESIAN_POINT('Ctrl Pts',(13.8932328528421,-0.214162491453186,
4.40474604470388));
#50728=CARTESIAN_POINT('Ctrl Pts',(13.8854871380565,-0.148524681204106,
4.43947685223224));
#50729=CARTESIAN_POINT('Ctrl Pts',(13.8777414232708,-0.0742589286223064,
4.45790169736071));
#50730=CARTESIAN_POINT('Ctrl Pts',(13.8699957084852,1.23414887176878E-6,
4.4579133809027));
#50731=CARTESIAN_POINT('Ctrl Pts',(13.9800042915148,-4.68615130337092E-6,
4.45784092071359));
#50732=CARTESIAN_POINT('Ctrl Pts',(13.9833817079953,-0.0323996211791616,
4.45785275579335));
#50733=CARTESIAN_POINT('Ctrl Pts',(13.9867591244758,-0.064792114138131,
4.45446164082457));
#50734=CARTESIAN_POINT('Ctrl Pts',(13.9901365409563,-0.0964458636128916,
4.44764173788363));
#50735=CARTESIAN_POINT('Ctrl Pts',(13.9980079130062,-0.170217765992045,
4.43174734235885));
#50736=CARTESIAN_POINT('Ctrl Pts',(14.0058792850562,-0.239977073556624,
4.39722897636055));
#50737=CARTESIAN_POINT('Ctrl Pts',(14.0137506571061,-0.297364634468633,
4.34822292324149));
#50738=CARTESIAN_POINT('Ctrl Pts',(14.0216220291561,-0.354752195380644,
4.29921687012243));
#50739=CARTESIAN_POINT('Ctrl Pts',(14.0294934012061,-0.399768009640084,
4.23572312988262));
#50740=CARTESIAN_POINT('Ctrl Pts',(14.037364773256,-0.427017900618165,4.16535006094698));
#50741=CARTESIAN_POINT('Ctrl Pts',(14.045236145306,-0.454267791596245,4.09497699201134));
#50742=CARTESIAN_POINT('Ctrl Pts',(14.0531075173559,-0.463751759292965,
4.01772459437987));
#50743=CARTESIAN_POINT('Ctrl Pts',(14.0609788894059,-0.45433335426851,3.94284990548881));
#50744=CARTESIAN_POINT('Ctrl Pts',(14.0688502614558,-0.444914949244056,
3.86797521659775));
#50745=CARTESIAN_POINT('Ctrl Pts',(14.0767216335058,-0.416594171498428,
3.7954782364471));
#50746=CARTESIAN_POINT('Ctrl Pts',(14.0845930055557,-0.372764656800254,
3.7340461680214));
#50747=CARTESIAN_POINT('Ctrl Pts',(14.0924643776057,-0.328935142102078,
3.67261409959569));
#50748=CARTESIAN_POINT('Ctrl Pts',(14.1003357496557,-0.269596890451354,
3.62224694289495));
#50749=CARTESIAN_POINT('Ctrl Pts',(14.1082071217056,-0.201860314388951,
3.58898011778223));
#50750=CARTESIAN_POINT('Ctrl Pts',(14.1160784937556,-0.134123738326549,
3.55571329266952));
#50751=CARTESIAN_POINT('Ctrl Pts',(14.1239498658055,-0.0579888378524715,
3.53954679914483));
#50752=CARTESIAN_POINT('Ctrl Pts',(14.1318212378555,0.0174212575835846,
3.54241784356498));
#50753=CARTESIAN_POINT('Ctrl Pts',(14.1396926099054,0.0928313530196406,
3.54528888798513));
#50754=CARTESIAN_POINT('Ctrl Pts',(14.1475639819554,0.167516643417675,3.56719747035013));
#50755=CARTESIAN_POINT('Ctrl Pts',(14.1554353540053,0.232527703900953,3.60551831852155));
#50756=CARTESIAN_POINT('Ctrl Pts',(14.1633067260553,0.297538764384231,3.64383916669297));
#50757=CARTESIAN_POINT('Ctrl Pts',(14.1711780981053,0.352875594952755,3.69857228067082));
#50758=CARTESIAN_POINT('Ctrl Pts',(14.1790494701552,0.391907267274456,3.76315907456484));
#50759=CARTESIAN_POINT('Ctrl Pts',(14.1869208422052,0.430938939596158,3.82774586845886));
#50760=CARTESIAN_POINT('Ctrl Pts',(14.1947922142551,0.453665453671035,3.90218634226906));
#50761=CARTESIAN_POINT('Ctrl Pts',(14.2026635863051,0.45736352584659,3.97756040711846));
#50762=CARTESIAN_POINT('Ctrl Pts',(14.210534958355,0.461061598022145,4.05293447196787));
#50763=CARTESIAN_POINT('Ctrl Pts',(14.218406330405,0.445731228298378,4.12924212785648));
#50764=CARTESIAN_POINT('Ctrl Pts',(14.2262777024549,0.413209431587385,4.19733954431574));
#50765=CARTESIAN_POINT('Ctrl Pts',(14.2341490745049,0.380687634876391,4.265436960775));
#50766=CARTESIAN_POINT('Ctrl Pts',(14.2420204465549,0.330974411178171,4.32532413780492));
#50767=CARTESIAN_POINT('Ctrl Pts',(14.2498918186048,0.270026820557645,4.36982488597043));
#50768=CARTESIAN_POINT('Ctrl Pts',(14.2577631906548,0.209079229937118,4.41432563413594));
#50769=CARTESIAN_POINT('Ctrl Pts',(14.2656345627047,0.136897272394287,4.44343995343705));
#50770=CARTESIAN_POINT('Ctrl Pts',(14.2735059347547,0.0621304022332317,
4.45367911922619));
#50771=CARTESIAN_POINT('Ctrl Pts',(14.2756720536747,0.0415553447945806,
4.4564968301158));
#50772=CARTESIAN_POINT('Ctrl Pts',(14.2778381725948,0.020784533837212,4.45788513960506));
#50773=CARTESIAN_POINT('Ctrl Pts',(14.2800042915148,1.11332528513013E-5,
4.45786561359635));
#50774=CARTESIAN_POINT('Origin',(12.5,0.,4.));
#50775=CARTESIAN_POINT('',(14.5800042915148,-1.58578451148518E-6,4.45791318879952));
#50776=CARTESIAN_POINT('',(14.4699957084852,4.96934848862042E-6,4.4578413260902));
#50777=CARTESIAN_POINT('',(12.5,-5.60735153159594E-17,4.457875));
#50778=CARTESIAN_POINT('Ctrl Pts',(14.4699957084852,4.96934848862042E-6,
4.4578413260902));
#50779=CARTESIAN_POINT('Ctrl Pts',(14.4666543524698,0.0320539454002899,
4.45785375637851));
#50780=CARTESIAN_POINT('Ctrl Pts',(14.4633129964543,0.0641003838712636,
4.45453523052653));
#50781=CARTESIAN_POINT('Ctrl Pts',(14.4599716404389,0.0954313752779353,
4.44785911407655));
#50782=CARTESIAN_POINT('Ctrl Pts',(14.452100268389,0.169239101517837,4.43213190746217));
#50783=CARTESIAN_POINT('Ctrl Pts',(14.444228896339,0.2390764403586,4.39777168651743));
#50784=CARTESIAN_POINT('Ctrl Pts',(14.4363575242891,0.296574889592956,4.34889578431359));
#50785=CARTESIAN_POINT('Ctrl Pts',(14.4284861522391,0.354073338827311,4.30001988210975));
#50786=CARTESIAN_POINT('Ctrl Pts',(14.4206147801891,0.39923289845526,4.2366282986468));
#50787=CARTESIAN_POINT('Ctrl Pts',(14.4127434081392,0.4266421670589,4.16631715105832));
#50788=CARTESIAN_POINT('Ctrl Pts',(14.4048720360892,0.454051435662541,4.09600600346984));
#50789=CARTESIAN_POINT('Ctrl Pts',(14.3970006640393,0.463710413241873,4.01877529175582));
#50790=CARTESIAN_POINT('Ctrl Pts',(14.3891292919893,0.454461679188747,3.94387945476197));
#50791=CARTESIAN_POINT('Ctrl Pts',(14.3812579199394,0.445212945135621,3.86898361776811));
#50792=CARTESIAN_POINT('Ctrl Pts',(14.3733865478894,0.417056499450037,3.79642265549441));
#50793=CARTESIAN_POINT('Ctrl Pts',(14.3655151758395,0.373366286239542,3.73489143780602));
#50794=CARTESIAN_POINT('Ctrl Pts',(14.3576438037895,0.329676073029047,3.67336022011762));
#50795=CARTESIAN_POINT('Ctrl Pts',(14.3497724317395,0.270452092293641,3.62285874701452));
#50796=CARTESIAN_POINT('Ctrl Pts',(14.3419010596896,0.202791063664024,3.58943853329022));
#50797=CARTESIAN_POINT('Ctrl Pts',(14.3340296876396,0.135130035034407,3.55601831956592));
#50798=CARTESIAN_POINT('Ctrl Pts',(14.3261583155897,0.0590319585105798,
3.53967936522043));
#50799=CARTESIAN_POINT('Ctrl Pts',(14.3182869435397,-0.0163844490157649,
3.54237954232867));
#50800=CARTESIAN_POINT('Ctrl Pts',(14.3104155714898,-0.0918008565421096,
3.54507971943691));
#50801=CARTESIAN_POINT('Ctrl Pts',(14.3025441994398,-0.166535595070972,
3.56681902799889));
#50802=CARTESIAN_POINT('Ctrl Pts',(14.2946728273899,-0.231633314431234,
3.60499247969884));
#50803=CARTESIAN_POINT('Ctrl Pts',(14.2868014553399,-0.296731033791496,
3.64316593139879));
#50804=CARTESIAN_POINT('Ctrl Pts',(14.2789300832899,-0.352191733983158,
3.6977735262367));
#50805=CARTESIAN_POINT('Ctrl Pts',(14.27105871124,-0.391369643565407,3.76227171909014));
#50806=CARTESIAN_POINT('Ctrl Pts',(14.26318733919,-0.430547553147657,3.82676991194359));
#50807=CARTESIAN_POINT('Ctrl Pts',(14.2553159671401,-0.453442672120494,
3.90115870281258));
#50808=CARTESIAN_POINT('Ctrl Pts',(14.2474445950901,-0.457311513162664,
3.97652419590847));
#50809=CARTESIAN_POINT('Ctrl Pts',(14.2395732230402,-0.461180354204834,
4.05188968900435));
#50810=CARTESIAN_POINT('Ctrl Pts',(14.2317018509902,-0.446022917316338,
4.12823188432714));
#50811=CARTESIAN_POINT('Ctrl Pts',(14.2238304789403,-0.413655495130362,
4.19640281260034));
#50812=CARTESIAN_POINT('Ctrl Pts',(14.2159591068903,-0.381288072944386,
4.26457374087354));
#50813=CARTESIAN_POINT('Ctrl Pts',(14.2080877348403,-0.33171066546093,4.32457340209717));
#50814=CARTESIAN_POINT('Ctrl Pts',(14.2002163627904,-0.270864058094251,
4.36921212802613));
#50815=CARTESIAN_POINT('Ctrl Pts',(14.1923449907404,-0.210017450727571,
4.41385085395509));
#50816=CARTESIAN_POINT('Ctrl Pts',(14.1844736186905,-0.137901643477669,
4.44312864458938));
#50817=CARTESIAN_POINT('Ctrl Pts',(14.1766022466405,-0.0631581639595259,
4.45353718675995));
#50818=CARTESIAN_POINT('Ctrl Pts',(14.1744000672554,-0.0422471272657682,
4.45644919204336));
#50819=CARTESIAN_POINT('Ctrl Pts',(14.1721978878703,-0.021130418320356,
4.45788427006097));
#50820=CARTESIAN_POINT('Ctrl Pts',(14.1699957084852,-1.10604184835328E-5,
4.4578646218584));
#50821=CARTESIAN_POINT('Ctrl Pts',(14.2800042915148,1.11332528513013E-5,
4.45786561359635));
#50822=CARTESIAN_POINT('Ctrl Pts',(14.2857095446447,-0.0547030874695854,
4.45781418483069));
#50823=CARTESIAN_POINT('Ctrl Pts',(14.2914147977746,-0.109435272994953,
4.44799629651036));
#50824=CARTESIAN_POINT('Ctrl Pts',(14.2971200509045,-0.16065599949712,4.42880599334559));
#50825=CARTESIAN_POINT('Ctrl Pts',(14.3049914229545,-0.231323748287136,
4.40232968939868));
#50826=CARTESIAN_POINT('Ctrl Pts',(14.3128627950045,-0.295307463087888,
4.35801306922771));
#50827=CARTESIAN_POINT('Ctrl Pts',(14.3207341670544,-0.344940072567234,
4.30116652609615));
#50828=CARTESIAN_POINT('Ctrl Pts',(14.3286055391044,-0.394572682046581,
4.24431998296459));
#50829=CARTESIAN_POINT('Ctrl Pts',(14.3364769111543,-0.429854186204522,
4.17494351687244));
#50830=CARTESIAN_POINT('Ctrl Pts',(14.3443482832043,-0.446556856002091,
4.10135040434572));
#50831=CARTESIAN_POINT('Ctrl Pts',(14.3522196552542,-0.46325952579966,4.027757291819));
#50832=CARTESIAN_POINT('Ctrl Pts',(14.3600910273042,-0.461383361236856,
3.9499475328577));
#50833=CARTESIAN_POINT('Ctrl Pts',(14.3679623993541,-0.441153180262727,
3.87724495265939));
#50834=CARTESIAN_POINT('Ctrl Pts',(14.3758337714041,-0.420922999288597,
3.80454237246108));
#50835=CARTESIAN_POINT('Ctrl Pts',(14.383705143454,-0.382338801903142,3.73694697102576));
#50836=CARTESIAN_POINT('Ctrl Pts',(14.391576515504,-0.330024073856894,3.68255860260764));
#50837=CARTESIAN_POINT('Ctrl Pts',(14.399447887554,-0.277709345810648,3.62817023418952));
#50838=CARTESIAN_POINT('Ctrl Pts',(14.4073192596039,-0.21166408710361,3.58698889878861));
#50839=CARTESIAN_POINT('Ctrl Pts',(14.4151906316539,-0.139802400742051,
3.56394929325792));
#50840=CARTESIAN_POINT('Ctrl Pts',(14.4230620037038,-0.0679407143804897,
3.54090968772722));
#50841=CARTESIAN_POINT('Ctrl Pts',(14.4309333757538,0.00973739963559066,
3.53601181206673));
#50842=CARTESIAN_POINT('Ctrl Pts',(14.4388047478037,0.0839238909224197,
3.54984257127538));
#50843=CARTESIAN_POINT('Ctrl Pts',(14.4466761198537,0.158110382209248,3.56367333048403));
#50844=CARTESIAN_POINT('Ctrl Pts',(14.4545474919037,0.228805250766822,3.59623272456181));
#50845=CARTESIAN_POINT('Ctrl Pts',(14.4624188639536,0.287537237904754,3.64361921078484));
#50846=CARTESIAN_POINT('Ctrl Pts',(14.4702902360036,0.346269225042686,3.69100569700788));
#50847=CARTESIAN_POINT('Ctrl Pts',(14.4781616080535,0.393038330760977,3.75321927537615));
#50848=CARTESIAN_POINT('Ctrl Pts',(14.4860329801035,0.422240284179214,3.8228049873169));
#50849=CARTESIAN_POINT('Ctrl Pts',(14.4939043521534,0.451442237597453,3.89239069925764));
#50850=CARTESIAN_POINT('Ctrl Pts',(14.5017757242034,0.463077038715637,3.96934854477086));
#50851=CARTESIAN_POINT('Ctrl Pts',(14.5096470962533,0.45575050699275,4.04445678215295));
#50852=CARTESIAN_POINT('Ctrl Pts',(14.5175184683033,0.448423975269863,4.11956501953505));
#50853=CARTESIAN_POINT('Ctrl Pts',(14.5253898403532,0.422136110705906,4.19282364878603));
#50854=CARTESIAN_POINT('Ctrl Pts',(14.5332612124032,0.380036948171907,4.2554541996672));
#50855=CARTESIAN_POINT('Ctrl Pts',(14.5411325844532,0.337937785637909,4.31808475054837));
#50856=CARTESIAN_POINT('Ctrl Pts',(14.5490039565031,0.28002732513387,4.37008722305972));
#50857=CARTESIAN_POINT('Ctrl Pts',(14.5568753285531,0.213244889156206,4.40523023992844));
#50858=CARTESIAN_POINT('Ctrl Pts',(14.5645849828737,0.147834501639678,4.43965124177167));
#50859=CARTESIAN_POINT('Ctrl Pts',(14.5722946371942,0.0739129441497101,
4.45789842831743));
#50860=CARTESIAN_POINT('Ctrl Pts',(14.5800042915148,-1.58578451148518E-6,
4.45791318879952));
#50861=CARTESIAN_POINT('Origin',(12.5,0.,4.));
#50862=CARTESIAN_POINT('',(14.8800042915148,-1.01702808208336E-5,4.45785711824254));
#50863=CARTESIAN_POINT('',(14.7699957084852,8.6346448269735E-6,4.45789857801605));
#50864=CARTESIAN_POINT('',(12.5,-5.60735153159594E-17,4.457875));
#50865=CARTESIAN_POINT('Ctrl Pts',(14.7699957084852,8.6346448269735E-6,
4.45789857801605));
#50866=CARTESIAN_POINT('Ctrl Pts',(14.7689821891192,0.00972641784825355,
4.45790700998655));
#50867=CARTESIAN_POINT('Ctrl Pts',(14.7679686697532,0.01944367562558,4.45760386164098));
#50868=CARTESIAN_POINT('Ctrl Pts',(14.7669551503872,0.0291408329004781,
4.45698549795522));
#50869=CARTESIAN_POINT('Ctrl Pts',(14.7590837783372,0.104452598317788,4.45218305332902));
#50870=CARTESIAN_POINT('Ctrl Pts',(14.7512124062873,0.178551969979598,4.4283678943965));
#50871=CARTESIAN_POINT('Ctrl Pts',(14.7433410342373,0.242559732875008,4.38839375563686));
#50872=CARTESIAN_POINT('Ctrl Pts',(14.7354696621874,0.30656749577042,4.34841961687722));
#50873=CARTESIAN_POINT('Ctrl Pts',(14.7275982901374,0.360483649899433,4.29228649829047));
#50874=CARTESIAN_POINT('Ctrl Pts',(14.7197269180875,0.397847504376097,4.22672074611392));
#50875=CARTESIAN_POINT('Ctrl Pts',(14.7118555460375,0.435211358852761,4.16115499393738));
#50876=CARTESIAN_POINT('Ctrl Pts',(14.7039841739875,0.456022913677073,4.08615660817103));
#50877=CARTESIAN_POINT('Ctrl Pts',(14.6961128019376,0.457788351878884,4.01071253147039));
#50878=CARTESIAN_POINT('Ctrl Pts',(14.6882414298876,0.459553790080695,3.93526845476975));
#50879=CARTESIAN_POINT('Ctrl Pts',(14.6803700578377,0.442273111660005,3.85937868713481));
#50880=CARTESIAN_POINT('Ctrl Pts',(14.6724986857877,0.408017034045316,3.79213698410258));
#50881=CARTESIAN_POINT('Ctrl Pts',(14.6646273137378,0.373760956430627,3.72489528107034));
#50882=CARTESIAN_POINT('Ctrl Pts',(14.6567559416878,0.32252947962194,3.6663016426408));
#50883=CARTESIAN_POINT('Ctrl Pts',(14.6488845696379,0.260461593653079,3.6233772554918));
#50884=CARTESIAN_POINT('Ctrl Pts',(14.6410131975879,0.198393707684219,3.5804528683428));
#50885=CARTESIAN_POINT('Ctrl Pts',(14.6331418255379,0.125489412555185,3.55319773247434));
#50886=CARTESIAN_POINT('Ctrl Pts',(14.625270453488,0.0504847191830214,3.54487778940425));
#50887=CARTESIAN_POINT('Ctrl Pts',(14.617399081438,-0.0245199741891427,
3.53655784633416));
#50888=CARTESIAN_POINT('Ctrl Pts',(14.6095277093881,-0.101625065804437,
3.54717309606245));
#50889=CARTESIAN_POINT('Ctrl Pts',(14.6016563373381,-0.171591169681571,
3.57545152934398));
#50890=CARTESIAN_POINT('Ctrl Pts',(14.5937849652882,-0.241557273558703,
3.6037299626255));
#50891=CARTESIAN_POINT('Ctrl Pts',(14.5859135932382,-0.304384389697674,
3.64967157946028));
#50892=CARTESIAN_POINT('Ctrl Pts',(14.5780422211883,-0.352544040227279,
3.70777126570269));
#50893=CARTESIAN_POINT('Ctrl Pts',(14.5701708491383,-0.400703690756885,
3.7658709519451));
#50894=CARTESIAN_POINT('Ctrl Pts',(14.5622994770883,-0.434195875677124,
3.83612870759516));
#50895=CARTESIAN_POINT('Ctrl Pts',(14.5544281050384,-0.449007277354457,
3.91012565253846));
#50896=CARTESIAN_POINT('Ctrl Pts',(14.5465567329884,-0.46381867903179,3.98412259748177));
#50897=CARTESIAN_POINT('Ctrl Pts',(14.5386853609385,-0.459949297466218,
4.06185873171832));
#50898=CARTESIAN_POINT('Ctrl Pts',(14.5308139888885,-0.437862794771992,
4.13401905238929));
#50899=CARTESIAN_POINT('Ctrl Pts',(14.5229426168386,-0.415776292077766,
4.20617937306026));
#50900=CARTESIAN_POINT('Ctrl Pts',(14.5150712447886,-0.375472668254887,
4.27276388016565));
#50901=CARTESIAN_POINT('Ctrl Pts',(14.5071998727387,-0.321781445311454,
4.32579385338299));
#50902=CARTESIAN_POINT('Ctrl Pts',(14.4993285006887,-0.26809022236802,4.37882382660034));
#50903=CARTESIAN_POINT('Ctrl Pts',(14.4914571286387,-0.201011400304033,
4.41829926592964));
#50904=CARTESIAN_POINT('Ctrl Pts',(14.4835857565888,-0.128582932452519,
4.43948988945229));
#50905=CARTESIAN_POINT('Ctrl Pts',(14.4790557405542,-0.0868999680795747,
4.45168520479633));
#50906=CARTESIAN_POINT('Ctrl Pts',(14.4745257245197,-0.0434451672832877,
4.45782447382869));
#50907=CARTESIAN_POINT('Ctrl Pts',(14.4699957084852,4.96934848862042E-6,
4.4578413260902));
#50908=CARTESIAN_POINT('Ctrl Pts',(14.5800042915148,-1.58578451148518E-6,
4.45791318879952));
#50909=CARTESIAN_POINT('Ctrl Pts',(14.5801660092442,-0.00155201715944126,
4.45791349841543));
#50910=CARTESIAN_POINT('Ctrl Pts',(14.5803277269736,-0.00310244544229786,
4.45790578589721));
#50911=CARTESIAN_POINT('Ctrl Pts',(14.5804894447029,-0.0046527920161852,
4.45789003224535));
#50912=CARTESIAN_POINT('Ctrl Pts',(14.5883608167529,-0.0801136257596197,
4.45712324646747));
#50913=CARTESIAN_POINT('Ctrl Pts',(14.5962321888029,-0.155380881795201,
4.43730611368561));
#50914=CARTESIAN_POINT('Ctrl Pts',(14.6041035608528,-0.22143539919095,4.4008132908088));
#50915=CARTESIAN_POINT('Ctrl Pts',(14.6119749329028,-0.287489916586699,
4.36432046793199));
#50916=CARTESIAN_POINT('Ctrl Pts',(14.6198463049527,-0.344331695342615,
4.31115195496024));
#50917=CARTESIAN_POINT('Ctrl Pts',(14.6277176770027,-0.38514947146564,4.24767885402976));
#50918=CARTESIAN_POINT('Ctrl Pts',(14.6355890490526,-0.425967247588666,
4.18420575309928));
#50919=CARTESIAN_POINT('Ctrl Pts',(14.6434604211026,-0.4507610210788,4.11042806421008));
#50920=CARTESIAN_POINT('Ctrl Pts',(14.6513317931525,-0.45655979174196,4.03518645571321));
#50921=CARTESIAN_POINT('Ctrl Pts',(14.6592031652025,-0.462358562405121,
3.95994484721634));
#50922=CARTESIAN_POINT('Ctrl Pts',(14.6670745372524,-0.449162330241309,
3.8832393191118));
#50923=CARTESIAN_POINT('Ctrl Pts',(14.6749459093024,-0.41855237967279,3.81426137832517));
#50924=CARTESIAN_POINT('Ctrl Pts',(14.6828172813524,-0.387942429104271,
3.74528343753854));
#50925=CARTESIAN_POINT('Ctrl Pts',(14.6906886534023,-0.339918760131043,
3.68403308406983));
#50926=CARTESIAN_POINT('Ctrl Pts',(14.6985600254523,-0.280235976103336,
3.63784985464301));
#50927=CARTESIAN_POINT('Ctrl Pts',(14.7064313975022,-0.220553192075631,
3.5916666252162));
#50928=CARTESIAN_POINT('Ctrl Pts',(14.7143027695522,-0.149211292993445,
3.5605505198313));
#50929=CARTESIAN_POINT('Ctrl Pts',(14.7221741416021,-0.0747590701011626,
3.54823013427646));
#50930=CARTESIAN_POINT('Ctrl Pts',(14.7300455136521,-0.000306847208877067,
3.53590974872161));
#50931=CARTESIAN_POINT('Ctrl Pts',(14.737916885702,0.0772556994935079,3.54238508299684));
#50932=CARTESIAN_POINT('Ctrl Pts',(14.745788257752,0.148634367597872,3.5668802073009));
#50933=CARTESIAN_POINT('Ctrl Pts',(14.753659629802,0.220013035702235,3.59137533160497));
#50934=CARTESIAN_POINT('Ctrl Pts',(14.7615310018519,0.285207825208577,3.63389024593787));
#50935=CARTESIAN_POINT('Ctrl Pts',(14.7694023739019,0.336406544142474,3.68933045342307));
#50936=CARTESIAN_POINT('Ctrl Pts',(14.7772737459518,0.387605263076371,3.74477066090827));
#50937=CARTESIAN_POINT('Ctrl Pts',(14.7851451180018,0.424807911437823,3.81313616154577));
#50938=CARTESIAN_POINT('Ctrl Pts',(14.7930164900517,0.443556551112275,3.88623481973509));
#50939=CARTESIAN_POINT('Ctrl Pts',(14.8008878621017,0.462305190786727,3.9593334779244));
#50940=CARTESIAN_POINT('Ctrl Pts',(14.8087592341516,0.462599821774179,4.03716529366552));
#50941=CARTESIAN_POINT('Ctrl Pts',(14.8166306062016,0.444405141642572,4.11040380200553));
#50942=CARTESIAN_POINT('Ctrl Pts',(14.8245019782516,0.426210461510966,4.18364231034555));
#50943=CARTESIAN_POINT('Ctrl Pts',(14.8323733503015,0.389526470260302,4.25228751128446));
#50944=CARTESIAN_POINT('Ctrl Pts',(14.8402447223515,0.338748948932789,4.3081137476731));
#50945=CARTESIAN_POINT('Ctrl Pts',(14.8481160944014,0.287971427605278,4.36393998406173));
#50946=CARTESIAN_POINT('Ctrl Pts',(14.8559874664514,0.22310037620092,4.40694725590009));
#50947=CARTESIAN_POINT('Ctrl Pts',(14.8638588385013,0.151909206873508,4.43198208217373));
#50948=CARTESIAN_POINT('Ctrl Pts',(14.8692406561725,0.103234351881841,4.44909890368578));
#50949=CARTESIAN_POINT('Ctrl Pts',(14.8746224738437,0.0516050086776526,
4.45781408155485));
#50950=CARTESIAN_POINT('Ctrl Pts',(14.8800042915148,-1.01702808208336E-5,
4.45785711824254));
#50951=CARTESIAN_POINT('Origin',(12.5,0.,4.));
#50952=CARTESIAN_POINT('',(15.1,-5.60735153159594E-17,4.457875));
#50953=CARTESIAN_POINT('',(15.0699957084852,-1.05870731373636E-5,4.45788944868556));
#50954=CARTESIAN_POINT('',(12.5,-5.60735153159594E-17,4.457875));
#50955=CARTESIAN_POINT('',(15.1,-0.269165465906718,4.37040446485999));
#50956=CARTESIAN_POINT('Origin',(15.1,0.,4.));
#50957=CARTESIAN_POINT('Ctrl Pts',(15.1,-0.269173508333955,4.37043259773194));
#50958=CARTESIAN_POINT('Ctrl Pts',(15.0991842588284,-0.262849866117432,
4.37503549456412));
#50959=CARTESIAN_POINT('Ctrl Pts',(15.0983685176569,-0.256407545646713,
4.37947450812006));
#50960=CARTESIAN_POINT('Ctrl Pts',(15.0975527764853,-0.249853611926923,
4.38374199825787));
#50961=CARTESIAN_POINT('Ctrl Pts',(15.0896814044354,-0.186612411779406,
4.42492050409441));
#50962=CARTESIAN_POINT('Ctrl Pts',(15.0818100323854,-0.112978907049287,
4.45012847221118));
#50963=CARTESIAN_POINT('Ctrl Pts',(15.0739386603355,-0.0377721395608013,
4.45635245505497));
#50964=CARTESIAN_POINT('Ctrl Pts',(15.072624343052,-0.0252145379490987,
4.45739170058566));
#50965=CARTESIAN_POINT('Ctrl Pts',(15.0713100257686,-0.0126130730861363,
4.45790166433459));
#50966=CARTESIAN_POINT('Ctrl Pts',(15.0699957084852,-1.05870731373636E-5,
4.45788944868556));
#50967=CARTESIAN_POINT('Origin',(11.8752146997001,0.,4.));
#50968=CARTESIAN_POINT('',(14.9247853002999,-1.38824472118437E-5,4.62497559137666));
#50969=CARTESIAN_POINT('',(15.0252146997001,-1.44513692928093E-5,4.62501972247551));
#50970=CARTESIAN_POINT('',(11.8752146997001,-1.68747709936658E-14,4.625));
#50971=CARTESIAN_POINT('',(15.1,-0.624993681275899,4.00281040303151));
#50972=CARTESIAN_POINT('Ctrl Pts',(15.0252146997001,-1.44513692928189E-5,
4.62501972247551));
#50973=CARTESIAN_POINT('Ctrl Pts',(15.0265290169835,-0.017216861979444,
4.62503639685311));
#50974=CARTESIAN_POINT('Ctrl Pts',(15.0357147063169,-0.137433797398843,
4.62017138475037));
#50975=CARTESIAN_POINT('Ctrl Pts',(15.0527717677003,-0.355236031271534,
4.54560815721762));
#50976=CARTESIAN_POINT('Ctrl Pts',(15.0763858838501,-0.571652475026301,
4.31158258982903));
#50977=CARTESIAN_POINT('Ctrl Pts',(15.09212862795,-0.624530364890795,4.10584538053252));
#50978=CARTESIAN_POINT('Ctrl Pts',(15.1,-0.624993681275899,4.00281040303152));
#50979=CARTESIAN_POINT('',(15.1,0.314930721058197,3.46014479632612));
#50980=CARTESIAN_POINT('Origin',(15.1,0.,4.));
#50981=CARTESIAN_POINT('Ctrl Pts',(14.9247853002999,-1.38824472118368E-5,
4.62497559137666));
#50982=CARTESIAN_POINT('Ctrl Pts',(14.9272748546787,-0.0326052931943186,
4.62500276606431));
#50983=CARTESIAN_POINT('Ctrl Pts',(14.9376357811074,-0.168225686180582,
4.61457389311938));
#50984=CARTESIAN_POINT('Ctrl Pts',(14.9558680795861,-0.394527586443172,
4.517903766532));
#50985=CARTESIAN_POINT('Ctrl Pts',(14.979482195736,-0.593077772790822,4.26857965265179));
#50986=CARTESIAN_POINT('Ctrl Pts',(15.0030963118859,-0.649493436571599,
3.95488773069898));
#50987=CARTESIAN_POINT('Ctrl Pts',(15.0267104280357,-0.550252000240565,
3.65200904506483));
#50988=CARTESIAN_POINT('Ctrl Pts',(15.0503245441856,-0.319142060764588,
3.43252503194012));
#50989=CARTESIAN_POINT('Ctrl Pts',(15.0739386603355,-0.0115409051696555,
3.34904846156061));
#50990=CARTESIAN_POINT('Ctrl Pts',(15.0904971456069,0.20608092381284,3.39989411918499));
#50991=CARTESIAN_POINT('Ctrl Pts',(15.0991842588284,0.305720220830039,3.45471854406458));
#50992=CARTESIAN_POINT('Ctrl Pts',(15.1,0.314937815442301,3.46010549098218));
#50993=CARTESIAN_POINT('Origin',(11.8752146997001,0.,4.));
#50994=CARTESIAN_POINT('',(14.6247853002999,-2.16459804047719E-6,4.62505212776347));
#50995=CARTESIAN_POINT('',(14.7252146997001,1.17863019661874E-5,4.62503218402409));
#50996=CARTESIAN_POINT('',(11.8752146997001,-1.68747709936658E-14,4.625));
#50997=CARTESIAN_POINT('Ctrl Pts',(14.7252146997001,1.17863019662174E-5,
4.62503218402409));
#50998=CARTESIAN_POINT('Ctrl Pts',(14.7320725523841,-0.0897427467603322,
4.62495430540108));
#50999=CARTESIAN_POINT('Ctrl Pts',(14.746801777118,-0.282587126126967,4.58296482291278));
#51000=CARTESIAN_POINT('Ctrl Pts',(14.7694023739019,-0.520130285395982,
4.39158760667368));
#51001=CARTESIAN_POINT('Ctrl Pts',(14.7930164900517,-0.64367318065081,4.09778141619902));
#51002=CARTESIAN_POINT('Ctrl Pts',(14.8166306062016,-0.612955311082805,
3.78054123783642));
#51003=CARTESIAN_POINT('Ctrl Pts',(14.8402447223515,-0.435338447621071,
3.51589585985611));
#51004=CARTESIAN_POINT('Ctrl Pts',(14.8638588385013,-0.153389665944836,
3.36726945127358));
#51005=CARTESIAN_POINT('Ctrl Pts',(14.8874729546512,0.165319955489652,3.37028123293502));
#51006=CARTESIAN_POINT('Ctrl Pts',(14.9110870708011,0.444409630539555,3.52420969451069));
#51007=CARTESIAN_POINT('Ctrl Pts',(14.9347011869509,0.616993161964042,3.79216419995926));
#51008=CARTESIAN_POINT('Ctrl Pts',(14.9583153031008,0.641710593195818,4.10992889087348));
#51009=CARTESIAN_POINT('Ctrl Pts',(14.9819294192507,0.512636325700993,4.40134645341462));
#51010=CARTESIAN_POINT('Ctrl Pts',(15.0042292181171,0.274729866520086,4.58571614948967));
#51011=CARTESIAN_POINT('Ctrl Pts',(15.0186576449336,0.0858074045169303,
4.62493653494651));
#51012=CARTESIAN_POINT('Ctrl Pts',(15.0252146997001,-1.44513692928189E-5,
4.62501972247551));
#51013=CARTESIAN_POINT('Ctrl Pts',(14.6247853002999,-2.16459804049194E-6,
4.62505212776347));
#51014=CARTESIAN_POINT('Ctrl Pts',(14.6249470180292,-0.00211850554115318,
4.62505255038961));
#51015=CARTESIAN_POINT('Ctrl Pts',(14.6329801078086,-0.107244412024774,
4.62452960748548));
#51016=CARTESIAN_POINT('Ctrl Pts',(14.6488845696379,-0.314835022974042,
4.56987302880665));
#51017=CARTESIAN_POINT('Ctrl Pts',(14.6724986857877,-0.547602339746838,
4.35214775046202));
#51018=CARTESIAN_POINT('Ctrl Pts',(14.6961128019376,-0.649132943719538,
4.05002781234082));
#51019=CARTESIAN_POINT('Ctrl Pts',(14.7197269180875,-0.595094318970103,
3.73591836064326));
#51020=CARTESIAN_POINT('Ctrl Pts',(14.7433410342373,-0.398437197867616,
3.48509791236843));
#51021=CARTESIAN_POINT('Ctrl Pts',(14.7669551503872,-0.1062918289807,3.35767733339665));
#51022=CARTESIAN_POINT('Ctrl Pts',(14.7905692665371,0.211327117384507,3.38419385377023));
#51023=CARTESIAN_POINT('Ctrl Pts',(14.8141833826869,0.478300047385911,3.5582926020622));
#51024=CARTESIAN_POINT('Ctrl Pts',(14.8377974988368,0.630645044771057,3.83824960712979));
#51025=CARTESIAN_POINT('Ctrl Pts',(14.8614116149867,0.631851559871185,4.15697121131127));
#51026=CARTESIAN_POINT('Ctrl Pts',(14.8850257311365,0.481630465478622,4.4380735902585));
#51027=CARTESIAN_POINT('Ctrl Pts',(14.9061502929076,0.243989509668873,4.59562135563586));
#51028=CARTESIAN_POINT('Ctrl Pts',(14.9194034826287,0.0704409072858971,
4.62491684623921));
#51029=CARTESIAN_POINT('Ctrl Pts',(14.9247853002999,-1.38824472118368E-5,
4.62497559137666));
#51030=CARTESIAN_POINT('Origin',(11.8752146997001,0.,4.));
#51031=CARTESIAN_POINT('',(14.3247853002999,1.51969053300144E-5,4.6249871875462));
#51032=CARTESIAN_POINT('',(14.4252146997001,6.78316748347314E-6,4.62495403506715));
#51033=CARTESIAN_POINT('',(11.8752146997001,-1.68747709936658E-14,4.625));
#51034=CARTESIAN_POINT('Ctrl Pts',(14.4252146997001,6.78316748347826E-6,
4.62495403506715));
#51035=CARTESIAN_POINT('Ctrl Pts',(14.4297447157347,-0.0593027126443913,
4.62493103170719));
#51036=CARTESIAN_POINT('Ctrl Pts',(14.4421461038192,-0.221686029527806,
4.60198961095629));
#51037=CARTESIAN_POINT('Ctrl Pts',(14.4624188639536,-0.457506203155893,
4.46321101183598));
#51038=CARTESIAN_POINT('Ctrl Pts',(14.4860329801035,-0.622549707754089,
4.19054718257559));
#51039=CARTESIAN_POINT('Ctrl Pts',(14.5096470962533,-0.63839484111024,3.87221739454711));
#51040=CARTESIAN_POINT('Ctrl Pts',(14.5332612124032,-0.501244206711231,
3.58451159745434));
#51041=CARTESIAN_POINT('Ctrl Pts',(14.5568753285531,-0.243966908844842,
3.39638048838484));
#51042=CARTESIAN_POINT('Ctrl Pts',(14.5804894447029,0.0717787570654544,
3.35291099727801));
#51043=CARTESIAN_POINT('Ctrl Pts',(14.6041035608528,0.370322144162233,3.46452089026927));
#51044=CARTESIAN_POINT('Ctrl Pts',(14.6277176770027,0.580115251486915,3.70446207957941));
#51045=CARTESIAN_POINT('Ctrl Pts',(14.6513317931525,0.650879700384091,4.0152309888134));
#51046=CARTESIAN_POINT('Ctrl Pts',(14.6749459093024,0.565656298155129,4.32234968564526));
#51047=CARTESIAN_POINT('Ctrl Pts',(14.6985600254523,0.344869426209941,4.55221503612336));
#51048=CARTESIAN_POINT('Ctrl Pts',(14.7153162889182,0.129554394067723,4.62141618582314));
#51049=CARTESIAN_POINT('Ctrl Pts',(14.7242011803341,0.0132765736394338,
4.62504369367533));
#51050=CARTESIAN_POINT('Ctrl Pts',(14.7252146997001,1.17863019662174E-5,
4.62503218402409));
#51051=CARTESIAN_POINT('Ctrl Pts',(14.3247853002999,1.51969053300109E-5,
4.6249871875462));
#51052=CARTESIAN_POINT('Ctrl Pts',(14.3304905534298,-0.0746697890657793,
4.62491698721088));
#51053=CARTESIAN_POINT('Ctrl Pts',(14.3440671786096,-0.252453835406249,
4.59302599116618));
#51054=CARTESIAN_POINT('Ctrl Pts',(14.3655151758395,-0.490432948250941,
4.42819608115853));
#51055=CARTESIAN_POINT('Ctrl Pts',(14.3891292919893,-0.634910852255616,
4.14409916841427));
#51056=CARTESIAN_POINT('Ctrl Pts',(14.4127434081392,-0.627227950688033,
3.82546788683648));
#51057=CARTESIAN_POINT('Ctrl Pts',(14.4363575242891,-0.469225504392149,
3.54866444115539));
#51058=CARTESIAN_POINT('Ctrl Pts',(14.4599716404389,-0.198769899531221,
3.38002670405092));
#51059=CARTESIAN_POINT('Ctrl Pts',(14.4835857565888,0.11932229545683,3.35996988316441));
#51060=CARTESIAN_POINT('Ctrl Pts',(14.5071998727387,0.408818071695872,3.49330073524378));
#51061=CARTESIAN_POINT('Ctrl Pts',(14.5308139888885,0.600337751131954,3.74806559342675));
#51062=CARTESIAN_POINT('Ctrl Pts',(14.5544281050384,0.647982309355475,4.06320828594604));
#51063=CARTESIAN_POINT('Ctrl Pts',(14.5780422211883,0.540333396317157,4.36320267272319));
#51064=CARTESIAN_POINT('Ctrl Pts',(14.6014946196088,0.304813865567294,4.57469465218781));
#51065=CARTESIAN_POINT('Ctrl Pts',(14.6170756459793,0.100891269655612,4.62503197968527));
#51066=CARTESIAN_POINT('Ctrl Pts',(14.6247853002999,-2.16459804049194E-6,
4.62505212776347));
#51067=CARTESIAN_POINT('Origin',(11.8752146997001,0.,4.));
#51068=CARTESIAN_POINT('',(14.0247853002999,-6.3966029390794E-6,4.62495348172753));
#51069=CARTESIAN_POINT('',(14.1252146997001,-1.50974863142078E-5,4.62498583382255));
#51070=CARTESIAN_POINT('',(11.8752146997001,-1.68747709936658E-14,4.625));
#51071=CARTESIAN_POINT('Ctrl Pts',(14.1252146997001,-1.50974863141889E-5,
4.62498583382255));
#51072=CARTESIAN_POINT('Ctrl Pts',(14.1274168790852,-0.0288430498503269,
4.62501265364587));
#51073=CARTESIAN_POINT('Ctrl Pts',(14.1374904305203,-0.160695812902997,
4.61605202430223));
#51074=CARTESIAN_POINT('Ctrl Pts',(14.1554353540053,-0.385112282251534,
4.52494275637564));
#51075=CARTESIAN_POINT('Ctrl Pts',(14.1790494701552,-0.588131968915973,
4.27924389796604));
#51076=CARTESIAN_POINT('Ctrl Pts',(14.2026635863051,-0.65020173504413,3.96662229549764));
#51077=CARTESIAN_POINT('Ctrl Pts',(14.2262777024549,-0.556446129094758,
3.66199989226673));
#51078=CARTESIAN_POINT('Ctrl Pts',(14.2498918186048,-0.329334334698108,
3.43838156778717));
#51079=CARTESIAN_POINT('Ctrl Pts',(14.2735059347547,-0.0232952743833569,
3.34935901020328));
#51080=CARTESIAN_POINT('Ctrl Pts',(14.2971200509045,0.28832666060365,3.41626709515619));
#51081=CARTESIAN_POINT('Ctrl Pts',(14.3207341670544,0.530849104237583,3.62307083431711));
#51082=CARTESIAN_POINT('Ctrl Pts',(14.3443482832043,0.646149864620809,3.92020827196535));
#51083=CARTESIAN_POINT('Ctrl Pts',(14.3679623993541,0.606596311879891,4.2364683526943));
#51084=CARTESIAN_POINT('Ctrl Pts',(14.391576515504,0.42166773027486,4.49605714656388));
#51085=CARTESIAN_POINT('Ctrl Pts',(14.4106606156193,0.190545343529355,4.60977018898031));
#51086=CARTESIAN_POINT('Ctrl Pts',(14.4218733436847,0.0437536792250838,
4.62497100242767));
#51087=CARTESIAN_POINT('Ctrl Pts',(14.4252146997001,6.78316748347826E-6,
4.62495403506715));
#51088=CARTESIAN_POINT('Ctrl Pts',(14.0247853002999,-6.39660293913491E-6,
4.62495348172753));
#51089=CARTESIAN_POINT('Ctrl Pts',(14.0281627167804,-0.0442255271350925,
4.62496963662755));
#51090=CARTESIAN_POINT('Ctrl Pts',(14.0394115053108,-0.191490205391595,
4.6095527480466));
#51091=CARTESIAN_POINT('Ctrl Pts',(14.0585316658912,-0.422790583021024,
4.49510047824495));
#51092=CARTESIAN_POINT('Ctrl Pts',(14.0821457820411,-0.60713052675338,4.23509335195577));
#51093=CARTESIAN_POINT('Ctrl Pts',(14.1057598981909,-0.645967413308333,
3.91874446730605));
#51094=CARTESIAN_POINT('Ctrl Pts',(14.1293740143408,-0.529993712466286,
3.62186903671368));
#51095=CARTESIAN_POINT('Ctrl Pts',(14.1529881304907,-0.287003328966194,
3.41561532377041));
#51096=CARTESIAN_POINT('Ctrl Pts',(14.1766022466405,0.0247694002478971,
3.34941346658496));
#51097=CARTESIAN_POINT('Ctrl Pts',(14.2002163627904,0.330605970264406,3.43912920108534));
#51098=CARTESIAN_POINT('Ctrl Pts',(14.2238304789403,0.557210518047066,3.66326152695696));
#51099=CARTESIAN_POINT('Ctrl Pts',(14.2474445950901,0.650275686248857,3.96809557204375));
#51100=CARTESIAN_POINT('Ctrl Pts',(14.27105871124,0.587497759452106,4.28057573538778));
#51101=CARTESIAN_POINT('Ctrl Pts',(14.2946728273899,0.383921904832036,4.52581397056352));
#51102=CARTESIAN_POINT('Ctrl Pts',(14.3125816904098,0.159750963363977,4.61623247111552));
#51103=CARTESIAN_POINT('Ctrl Pts',(14.3226191813798,0.0283709170587055,
4.62501384057475));
#51104=CARTESIAN_POINT('Ctrl Pts',(14.3247853002999,1.51969053300109E-5,
4.6249871875462));
#51105=CARTESIAN_POINT('Origin',(11.8752146997001,0.,4.));
#51106=CARTESIAN_POINT('',(13.7247853002999,-1.20831421157597E-5,4.62503091248755));
#51107=CARTESIAN_POINT('',(13.8252146997001,1.68461488569462E-6,4.62505238998457));
#51108=CARTESIAN_POINT('',(11.8752146997001,-1.68747709936658E-14,4.625));
#51109=CARTESIAN_POINT('Ctrl Pts',(13.8252146997001,1.68461488569581E-6,
4.62505238998457));
#51110=CARTESIAN_POINT('Ctrl Pts',(13.8329604144858,-0.101363538932993,
4.62503644193381));
#51111=CARTESIAN_POINT('Ctrl Pts',(13.8485775013214,-0.305753798836605,
4.57432856173903));
#51112=CARTESIAN_POINT('Ctrl Pts',(13.8720659602069,-0.541154937947787,
4.36197748624323));
#51113=CARTESIAN_POINT('Ctrl Pts',(13.8956800763568,-0.648123865072376,
4.06173996222779));
#51114=CARTESIAN_POINT('Ctrl Pts',(13.9192941925067,-0.599765396122921,
3.74670602647169));
#51115=CARTESIAN_POINT('Ctrl Pts',(13.9429083086565,-0.407668974822819,
3.49237575473668));
#51116=CARTESIAN_POINT('Ctrl Pts',(13.9665224248064,-0.117871845784803,
3.35970116712309));
#51117=CARTESIAN_POINT('Ctrl Pts',(13.9901365409563,0.200174091641329,3.38047865214521));
#51118=CARTESIAN_POINT('Ctrl Pts',(14.0137506571061,0.470246914526057,3.54972874087838));
#51119=CARTESIAN_POINT('Ctrl Pts',(14.037364773256,0.627621790796785,3.82688947135059));
#51120=CARTESIAN_POINT('Ctrl Pts',(14.0609788894059,0.634582735815489,4.14553734509456));
#51121=CARTESIAN_POINT('Ctrl Pts',(14.0845930055557,0.489461510650943,4.42930618095194));
#51122=CARTESIAN_POINT('Ctrl Pts',(14.1060049423205,0.251510284961593,4.59332024860173));
#51123=CARTESIAN_POINT('Ctrl Pts',(14.1195455070353,0.074198300926532,4.62491679006221));
#51124=CARTESIAN_POINT('Ctrl Pts',(14.1252146997001,-1.50974863141889E-5,
4.62498583382255));
#51125=CARTESIAN_POINT('Ctrl Pts',(13.7247853002999,-1.20831421156938E-5,
4.62503091248755));
#51126=CARTESIAN_POINT('Ctrl Pts',(13.7258348801309,-0.013748904810447,
4.62504304225186));
#51127=CARTESIAN_POINT('Ctrl Pts',(13.734755832012,-0.130498998332177,4.62127102305724));
#51128=CARTESIAN_POINT('Ctrl Pts',(13.7515481559429,-0.346119716157775,
4.55143222859795));
#51129=CARTESIAN_POINT('Ctrl Pts',(13.7751622720928,-0.566385203513325,
4.32106722332061));
#51130=CARTESIAN_POINT('Ctrl Pts',(13.7987763882427,-0.650912534047929,
4.01375622291695));
#51131=CARTESIAN_POINT('Ctrl Pts',(13.8223905043925,-0.57944414457563,3.70314844792952));
#51132=CARTESIAN_POINT('Ctrl Pts',(13.8460046205424,-0.369107932149097,
3.46368321387984));
#51133=CARTESIAN_POINT('Ctrl Pts',(13.8696187366923,-0.0703124342978696,
3.35275003110641));
#51134=CARTESIAN_POINT('Ctrl Pts',(13.8932328528421,0.245333927901481,3.3969348091043));
#51135=CARTESIAN_POINT('Ctrl Pts',(13.916846968992,0.502184306426786,3.58564835824111));
#51136=CARTESIAN_POINT('Ctrl Pts',(13.9404610851419,0.638682720042094,3.87366416276737));
#51137=CARTESIAN_POINT('Ctrl Pts',(13.9640752012917,0.62211637371287,4.19195723015293));
#51138=CARTESIAN_POINT('Ctrl Pts',(13.9876893174416,0.456455507660852,4.46424641105313));
#51139=CARTESIAN_POINT('Ctrl Pts',(14.007926017111,0.220741531225703,4.60224444133776));
#51140=CARTESIAN_POINT('Ctrl Pts',(14.0202913447304,0.058831122868106,4.62493198618401));
#51141=CARTESIAN_POINT('Ctrl Pts',(14.0247853002999,-6.39660293913491E-6,
4.62495348172753));
#51142=CARTESIAN_POINT('Origin',(11.8752146997001,0.,4.));
#51143=CARTESIAN_POINT('',(13.4247853002999,1.36962628664028E-5,4.62502243215823));
#51144=CARTESIAN_POINT('',(13.5252146997001,1.40828270379035E-5,4.62497680637469));
#51145=CARTESIAN_POINT('',(11.8752146997001,-1.68747709936658E-14,4.625));
#51146=CARTESIAN_POINT('Ctrl Pts',(13.5252146997001,1.4082827037902E-5,
4.62497680637469));
#51147=CARTESIAN_POINT('Ctrl Pts',(13.5306325778363,-0.0709123884867814,
4.62491668074428));
#51148=CARTESIAN_POINT('Ctrl Pts',(13.5439218280225,-0.244933372371362,
4.59533688876844));
#51149=CARTESIAN_POINT('Ctrl Pts',(13.5650824502587,-0.482621788093898,
4.43698120905743));
#51150=CARTESIAN_POINT('Ctrl Pts',(13.5886965664085,-0.632205603168059,
4.15553919999523));
#51151=CARTESIAN_POINT('Ctrl Pts',(13.6123106825584,-0.630276944445953,
3.83682113889318));
#51152=CARTESIAN_POINT('Ctrl Pts',(13.6359247987083,-0.477298028416376,
3.55721002779864));
#51153=CARTESIAN_POINT('Ctrl Pts',(13.6595389148582,-0.209931317243796,
3.38371661595291));
#51154=CARTESIAN_POINT('Ctrl Pts',(13.683153031008,0.107746895509167,3.35791980725116));
#51155=CARTESIAN_POINT('Ctrl Pts',(13.7067671471579,0.399602814690774,3.48600198647908));
#51156=CARTESIAN_POINT('Ctrl Pts',(13.7303812633077,0.59569113756138,3.73726736776131));
#51157=CARTESIAN_POINT('Ctrl Pts',(13.7539953794576,0.649017932507905,4.05149845333026));
#51158=CARTESIAN_POINT('Ctrl Pts',(13.7776094956075,0.546803061895555,4.35338757606046));
#51159=CARTESIAN_POINT('Ctrl Pts',(13.8012236117573,0.313543031018869,4.57058490613733));
#51160=CARTESIAN_POINT('Ctrl Pts',(13.8170920131216,0.106300066848774,4.6246481407235));
#51161=CARTESIAN_POINT('Ctrl Pts',(13.8250890424358,0.00164611344283092,
4.62505264870678));
#51162=CARTESIAN_POINT('Ctrl Pts',(13.8252146997001,1.68461488569581E-6,
4.62505238998457));
#51163=CARTESIAN_POINT('Ctrl Pts',(13.4247853002999,1.36962628664097E-5,
4.62502243215823));
#51164=CARTESIAN_POINT('Ctrl Pts',(13.4313784155315,-0.086279884022628,
4.62493973056585));
#51165=CARTESIAN_POINT('Ctrl Pts',(13.445842902813,-0.275670893367246,4.58538934244717));
#51166=CARTESIAN_POINT('Ctrl Pts',(13.4681787621445,-0.513544980480383,
4.40018484937968));
#51167=CARTESIAN_POINT('Ctrl Pts',(13.4917928782944,-0.64195771209056,4.10847422061066));
#51168=CARTESIAN_POINT('Ctrl Pts',(13.5154069944443,-0.616520809113462,
3.79076698974655));
#51169=CARTESIAN_POINT('Ctrl Pts',(13.5390211105941,-0.443330402422436,
3.52320390633144));
#51170=CARTESIAN_POINT('Ctrl Pts',(13.562635226744,-0.163892778617988,3.36990832590288));
#51171=CARTESIAN_POINT('Ctrl Pts',(13.5862493428939,0.154822890495328,3.36761860145296));
#51172=CARTESIAN_POINT('Ctrl Pts',(13.6098634590437,0.43643417612693,3.51688348138565));
#51173=CARTESIAN_POINT('Ctrl Pts',(13.6334775751936,0.613450973283793,3.78193059814177));
#51174=CARTESIAN_POINT('Ctrl Pts',(13.6570916913435,0.643449974253473,4.09923956510808));
#51175=CARTESIAN_POINT('Ctrl Pts',(13.6807058074933,0.519241709620395,4.39276507945606));
#51176=CARTESIAN_POINT('Ctrl Pts',(13.7032703438121,0.281645253009076,4.58329909926801));
#51177=CARTESIAN_POINT('Ctrl Pts',(13.717963508081,0.0892710189108511,4.62495207452848));
#51178=CARTESIAN_POINT('Ctrl Pts',(13.7247853002999,-1.20831421156938E-5,
4.62503091248755));
#51179=CARTESIAN_POINT('Origin',(11.8752146997001,0.,4.));
#51180=CARTESIAN_POINT('',(13.1247853002999,3.84888821539087E-6,4.62495078081483));
#51181=CARTESIAN_POINT('',(13.2252146997001,-9.32440196476731E-6,4.62495874418382));
#51182=CARTESIAN_POINT('',(11.8752146997001,-1.68747709936658E-14,4.625));
#51183=CARTESIAN_POINT('Ctrl Pts',(13.2252146997001,-9.32440196474427E-6,
4.62495874418382));
#51184=CARTESIAN_POINT('Ctrl Pts',(13.2283047411869,-0.040464997295585,
4.62498052751194));
#51185=CARTESIAN_POINT('Ctrl Pts',(13.2392661547237,-0.18396024524725,4.61125364372682));
#51186=CARTESIAN_POINT('Ctrl Pts',(13.2580989403104,-0.413782468289504,
4.50265339583901));
#51187=CARTESIAN_POINT('Ctrl Pts',(13.2817130564603,-0.602786876612853,
4.24601696851145));
#51188=CARTESIAN_POINT('Ctrl Pts',(13.3053271726101,-0.647329213752593,
3.9304208620728));
#51189=CARTESIAN_POINT('Ctrl Pts',(13.32894128876,-0.536734598538914,3.6314998804023));
#51190=CARTESIAN_POINT('Ctrl Pts',(13.3525554049099,-0.297507800394296,
3.42089251764738));
#51191=CARTESIAN_POINT('Ctrl Pts',(13.3761695210598,0.0130188131672444,
3.34907229440132));
#51192=CARTESIAN_POINT('Ctrl Pts',(13.3997836372096,0.320425377524893,3.43325142712992));
#51193=CARTESIAN_POINT('Ctrl Pts',(13.4233977533595,0.551039769569266,3.65325580067535));
#51194=CARTESIAN_POINT('Ctrl Pts',(13.4470118695093,0.649593644862141,3.95635983539258));
#51195=CARTESIAN_POINT('Ctrl Pts',(13.4706259856592,0.592467881122722,4.26992253935193));
#51196=CARTESIAN_POINT('Ctrl Pts',(13.4942401018091,0.393353065302923,4.5187964277335));
#51197=CARTESIAN_POINT('Ctrl Pts',(13.5124363398227,0.1672808180195,4.61476328251587));
#51198=CARTESIAN_POINT('Ctrl Pts',(13.5227612057864,0.0321332374692893,
4.62500403435298));
#51199=CARTESIAN_POINT('Ctrl Pts',(13.5252146997001,1.4082827037902E-5,
4.62497680637469));
#51200=CARTESIAN_POINT('Ctrl Pts',(13.1247853002999,3.84888821536311E-6,
4.62495078081483));
#51201=CARTESIAN_POINT('Ctrl Pts',(13.1290505788821,-0.0558403875021823,
4.6249385719914));
#51202=CARTESIAN_POINT('Ctrl Pts',(13.1411872295142,-0.214751600407627,
4.60383286368317));
#51203=CARTESIAN_POINT('Ctrl Pts',(13.1611952521963,-0.449738236712957,
4.47075670902068));
#51204=CARTESIAN_POINT('Ctrl Pts',(13.1848093683461,-0.619294173608025,
4.2008758003961));
#51205=CARTESIAN_POINT('Ctrl Pts',(13.208423484496,-0.64043195068177,3.88285360784221));
#51206=CARTESIAN_POINT('Ctrl Pts',(13.2320376006459,-0.508085752511173,
3.59290636366459));
#51207=CARTESIAN_POINT('Ctrl Pts',(13.2556517167957,-0.253973266794505,
3.40052194335125));
#51208=CARTESIAN_POINT('Ctrl Pts',(13.2792658329456,0.0610056803032868,
3.3518066124833));
#51209=CARTESIAN_POINT('Ctrl Pts',(13.3028799490955,0.361364191435218,3.45843533922715));
#51210=CARTESIAN_POINT('Ctrl Pts',(13.3264940652453,0.575119258511334,3.69485380694));
#51211=CARTESIAN_POINT('Ctrl Pts',(13.3501081813952,0.65104299168552,4.00440268404554));
#51212=CARTESIAN_POINT('Ctrl Pts',(13.3737222975451,0.570939739771795,4.31289642727099));
#51213=CARTESIAN_POINT('Ctrl Pts',(13.3973364136949,0.354006804717113,4.54640236352309));
#51214=CARTESIAN_POINT('Ctrl Pts',(13.4143574146132,0.136489422610972,4.62032507485564));
#51215=CARTESIAN_POINT('Ctrl Pts',(13.4235070434815,0.0167440814458925,
4.62503846613771));
#51216=CARTESIAN_POINT('Ctrl Pts',(13.4247853002999,1.36962628664097E-5,
4.62502243215823));
#51217=CARTESIAN_POINT('Origin',(11.8752146997001,0.,4.));
#51218=CARTESIAN_POINT('',(12.8247853002999,-1.55438223423121E-5,4.62499607812274));
#51219=CARTESIAN_POINT('',(12.9252146997001,-9.4222586321007E-6,4.62504029123831));
#51220=CARTESIAN_POINT('',(11.8752146997001,-1.68747709936658E-14,4.625));
#51221=CARTESIAN_POINT('Ctrl Pts',(12.9252146997001,-9.42225863212465E-6,
4.62504029123832));
#51222=CARTESIAN_POINT('Ctrl Pts',(12.9259769045375,-0.00998466834883174,
4.6250476064301));
#51223=CARTESIAN_POINT('Ctrl Pts',(12.9346104814248,-0.122971475467856,
4.62239759066569));
#51224=CARTESIAN_POINT('Ctrl Pts',(12.9511154303622,-0.336107011072318,
4.55759164674784));
#51225=CARTESIAN_POINT('Ctrl Pts',(12.974729546512,-0.56049590900091,4.33124115596169));
#51226=CARTESIAN_POINT('Ctrl Pts',(12.9983436626619,-0.650558060547343,
4.02550641626558));
#51227=CARTESIAN_POINT('Ctrl Pts',(13.0219577788117,-0.584709444123524,
3.71365888635357));
#51228=CARTESIAN_POINT('Ctrl Pts',(13.0455718949616,-0.378731139057797,
3.47043499764384));
#51229=CARTESIAN_POINT('Ctrl Pts',(13.0691860111115,-0.0819872800401352,
3.35412504823007));
#51230=CARTESIAN_POINT('Ctrl Pts',(13.0928001272613,0.234405401379786,3.39260352716186));
#51231=CARTESIAN_POINT('Ctrl Pts',(13.1164142434112,0.494621196584012,3.57664879910166));
#51232=CARTESIAN_POINT('Ctrl Pts',(13.1400283595611,0.636297578801308,3.86215313342763));
#51233=CARTESIAN_POINT('Ctrl Pts',(13.1636424757109,0.625480816776257,4.18069342892634));
#51234=CARTESIAN_POINT('Ctrl Pts',(13.1872565918608,0.464763222827219,4.45592928631477));
#51235=CARTESIAN_POINT('Ctrl Pts',(13.2077806665239,0.228267895462889,4.60018049807294));
#51236=CARTESIAN_POINT('Ctrl Pts',(13.220433369137,0.0625891701764018,4.62492503806923));
#51237=CARTESIAN_POINT('Ctrl Pts',(13.2252146997001,-9.32440196474427E-6,
4.62495874418382));
#51238=CARTESIAN_POINT('Ctrl Pts',(12.8247853002999,-1.55438223423052E-5,
4.62499607812274));
#51239=CARTESIAN_POINT('Ctrl Pts',(12.8267227422326,-0.0253767156259869,
4.62502109614712));
#51240=CARTESIAN_POINT('Ctrl Pts',(12.8365315562153,-0.153759343851268,
4.61735081595804));
#51241=CARTESIAN_POINT('Ctrl Pts',(12.854211742248,-0.376327535803878,4.5312757721487));
#51242=CARTESIAN_POINT('Ctrl Pts',(12.8778258583979,-0.583405888470749,
4.28898776831928));
#51243=CARTESIAN_POINT('Ctrl Pts',(12.9014399745477,-0.650666957548692,
3.97744183415536));
#51244=CARTESIAN_POINT('Ctrl Pts',(12.9250540906976,-0.561991161265395,
3.67130212143154));
#51245=CARTESIAN_POINT('Ctrl Pts',(12.9486682068475,-0.338630270727757,
3.44393714350224));
#51246=CARTESIAN_POINT('Ctrl Pts',(12.9722823229973,-0.0341142786054444,
3.34983650006563));
#51247=CARTESIAN_POINT('Ctrl Pts',(12.9958964391472,0.278577437919422,3.41155206540036));
#51248=CARTESIAN_POINT('Ctrl Pts',(13.0195105552971,0.524506132150044,3.61429327464512));
#51249=CARTESIAN_POINT('Ctrl Pts',(13.0431246714469,0.644733280558021,3.90947178565704));
#51250=CARTESIAN_POINT('Ctrl Pts',(13.0667387875968,0.61044561006836,4.22634601343335));
#51251=CARTESIAN_POINT('Ctrl Pts',(13.0903529037467,0.429860399609997,4.4889748434194));
#51252=CARTESIAN_POINT('Ctrl Pts',(13.1097017413144,0.197481915229314,4.60814700801091));
#51253=CARTESIAN_POINT('Ctrl Pts',(13.1211792068321,0.0472175377905832,
4.6249611028038));
#51254=CARTESIAN_POINT('Ctrl Pts',(13.1247853002999,3.84888821536311E-6,
4.62495078081483));
#51255=CARTESIAN_POINT('Origin',(11.8752146997001,0.,4.));
#51256=CARTESIAN_POINT('',(12.5247853002999,3.80998376854277E-6,4.62503871776264));
#51257=CARTESIAN_POINT('',(12.6252146997001,1.49489494596481E-5,4.6250110476872));
#51258=CARTESIAN_POINT('',(11.8752146997001,-1.68747709936658E-14,4.625));
#51259=CARTESIAN_POINT('',(12.5,0.310062960217711,4.54266560670548));
#51260=CARTESIAN_POINT('Ctrl Pts',(12.5,0.310062960217722,4.54266560670548));
#51261=CARTESIAN_POINT('Ctrl Pts',(12.50787137205,0.220600394030941,4.59378185169648));
#51262=CARTESIAN_POINT('Ctrl Pts',(12.5161331388166,0.113220056708515,4.6237347594226));
#51263=CARTESIAN_POINT('Ctrl Pts',(12.5243949055832,0.00511234815255113,
4.6250406321328));
#51264=CARTESIAN_POINT('Ctrl Pts',(12.5247853002999,3.80998376856706E-6,
4.62503871776264));
#51265=CARTESIAN_POINT('',(12.5,0.310062960217774,3.45733439329455));
#51266=CARTESIAN_POINT('Origin',(12.5,0.,4.));
#51267=CARTESIAN_POINT('Ctrl Pts',(12.5,0.310093463203755,3.45730861053195));
#51268=CARTESIAN_POINT('Ctrl Pts',(12.5008157411716,0.319367492808711,3.46259780682489));
#51269=CARTESIAN_POINT('Ctrl Pts',(12.5095028543931,0.416666480413896,3.52147574364868));
#51270=CARTESIAN_POINT('Ctrl Pts',(12.5260613396645,0.569511032758309,3.68451895614546));
#51271=CARTESIAN_POINT('Ctrl Pts',(12.5496754558144,0.651018771792273,3.99264764559437));
#51272=CARTESIAN_POINT('Ctrl Pts',(12.5732895719643,0.576495013506714,4.3025367374363));
#51273=CARTESIAN_POINT('Ctrl Pts',(12.5969036881141,0.363815091701307,4.53992168461618));
#51274=CARTESIAN_POINT('Ctrl Pts',(12.6142120640261,0.144017971622128,4.61907377583531));
#51275=CARTESIAN_POINT('Ctrl Pts',(12.6236490678881,0.0205077016108913,
4.62503160004571));
#51276=CARTESIAN_POINT('Ctrl Pts',(12.6252146997001,1.49489494596471E-5,
4.6250110476872));
#51277=CARTESIAN_POINT('Origin',(11.8752146997001,0.,4.));
#51278=CARTESIAN_POINT('Ctrl Pts',(12.6252146997001,1.49489494596471E-5,
4.6250110476872));
#51279=CARTESIAN_POINT('Ctrl Pts',(12.631520439938,-0.0825216819810338,
4.62492827098767));
#51280=CARTESIAN_POINT('Ctrl Pts',(12.6456975522259,-0.268159494659544,
4.5879440580038));
#51281=CARTESIAN_POINT('Ctrl Pts',(12.6677460365637,-0.506235857616531,
4.40939182910775));
#51282=CARTESIAN_POINT('Ctrl Pts',(12.6913601527136,-0.639894509617229,
4.12004729681268));
#51283=CARTESIAN_POINT('Ctrl Pts',(12.7149742688635,-0.620198095551099,
3.8019325752266));
#51284=CARTESIAN_POINT('Ctrl Pts',(12.7385883850133,-0.451866840211785,
3.53128609963859));
#51285=CARTESIAN_POINT('Ctrl Pts',(12.7622025011632,-0.17524257447904,3.37297016902465));
#51286=CARTESIAN_POINT('Ctrl Pts',(12.7858166173131,0.143379805101228,3.36492630429559));
#51287=CARTESIAN_POINT('Ctrl Pts',(12.809430733463,0.42764021116234,3.50908227080648));
#51288=CARTESIAN_POINT('Ctrl Pts',(12.8330448496128,0.609413666055986,3.77089008898231));
#51289=CARTESIAN_POINT('Ctrl Pts',(12.8566589657627,0.645136892431096,4.08760569204938));
#51290=CARTESIAN_POINT('Ctrl Pts',(12.8802730819125,0.526248572038732,4.38332598125533));
#51291=CARTESIAN_POINT('Ctrl Pts',(12.903124993225,0.289149347937084,4.5805996458561));
#51292=CARTESIAN_POINT('Ctrl Pts',(12.9181055324875,0.0930307802739178,
4.62497206165088));
#51293=CARTESIAN_POINT('Ctrl Pts',(12.9252146997001,-9.42225863212465E-6,
4.62504029123832));
#51294=CARTESIAN_POINT('Ctrl Pts',(12.5247853002999,3.80998376856706E-6,
4.62503871776264));
#51295=CARTESIAN_POINT('Ctrl Pts',(12.5322662776332,-0.0978890574527522,
4.62500203345524));
#51296=CARTESIAN_POINT('Ctrl Pts',(12.5476186270164,-0.298862923743373,
4.57698368148067));
#51297=CARTESIAN_POINT('Ctrl Pts',(12.5708423484496,-0.535054221536356,
4.37092866956447));
#51298=CARTESIAN_POINT('Ctrl Pts',(12.5944564645995,-0.647009713430093,
4.07251155115386));
#51299=CARTESIAN_POINT('Ctrl Pts',(12.6180705807493,-0.603894380709874,
3.75671714932517));
#51300=CARTESIAN_POINT('Ctrl Pts',(12.6416846968992,-0.416056506175611,
3.49922677321964));
#51301=CARTESIAN_POINT('Ctrl Pts',(12.6652988130491,-0.128505496873939,
3.36175035317655));
#51302=CARTESIAN_POINT('Ctrl Pts',(12.6889129291989,0.189841674427298,3.37723482234205));
#51303=CARTESIAN_POINT('Ctrl Pts',(12.7125270453488,0.462692468193658,3.54196933898577));
#51304=CARTESIAN_POINT('Ctrl Pts',(12.7361411614987,0.624655556881011,3.81647407445394));
#51305=CARTESIAN_POINT('Ctrl Pts',(12.7597552776485,0.636915702199809,4.13496208375113));
#51306=CARTESIAN_POINT('Ctrl Pts',(12.7833693937984,0.496534514683115,4.42110548633398));
#51307=CARTESIAN_POINT('Ctrl Pts',(12.8050460680155,0.258436396781676,4.5911312751119));
#51308=CARTESIAN_POINT('Ctrl Pts',(12.8188513701827,0.0776597756952025,
4.62491945378327));
#51309=CARTESIAN_POINT('Ctrl Pts',(12.8247853002999,-1.55438223423052E-5,
4.62499607812274));
#51310=CARTESIAN_POINT('Ctrl Pts',(12.5,-0.186196943290592,3.58169363627332));
#51311=CARTESIAN_POINT('Ctrl Pts',(12.50787137205,-0.117235947257613,3.55099764935784));
#51312=CARTESIAN_POINT('Ctrl Pts',(12.5236141161499,0.0360970477778841,
3.52440632583991));
#51313=CARTESIAN_POINT('Ctrl Pts',(12.5472282322997,0.257537368848111,3.59853698535937));
#51314=CARTESIAN_POINT('Ctrl Pts',(12.5708423484496,0.417223782598737,3.76887858727216));
#51315=CARTESIAN_POINT('Ctrl Pts',(12.5944564645995,0.476936352215019,3.99461366516243));
#51316=CARTESIAN_POINT('Ctrl Pts',(12.6180705807493,0.422340246895018,4.22163841384584));
#51317=CARTESIAN_POINT('Ctrl Pts',(12.6416846968992,0.266530936180377,4.39554662614981));
#51318=CARTESIAN_POINT('Ctrl Pts',(12.6652988130491,0.0468439715927196,
4.47465904879863));
#51319=CARTESIAN_POINT('Ctrl Pts',(12.6889129291989,-0.184068700558194,
4.44001626345752));
#51320=CARTESIAN_POINT('Ctrl Pts',(12.7125270453488,-0.37086838928987,4.29992045400434));
#51321=CARTESIAN_POINT('Ctrl Pts',(12.7361411614987,-0.468786717745582,
4.08794664964497));
#51322=CARTESIAN_POINT('Ctrl Pts',(12.7597552776485,-0.454357124800734,
3.85489580461101));
#51323=CARTESIAN_POINT('Ctrl Pts',(12.7833693937984,-0.331037647139153,
3.65662019659523));
#51324=CARTESIAN_POINT('Ctrl Pts',(12.8069835099483,-0.128382710063344,
3.54063794582746));
#51325=CARTESIAN_POINT('Ctrl Pts',(12.8305976260981,0.10504004521716,3.53474501052695));
#51326=CARTESIAN_POINT('Ctrl Pts',(12.854211742248,0.31328921869753,3.64035367159283));
#51327=CARTESIAN_POINT('Ctrl Pts',(12.8778258583979,0.446456451752615,3.83215407918844));
#51328=CARTESIAN_POINT('Ctrl Pts',(12.9014399745477,0.47262728739502,4.06417992999538));
#51329=CARTESIAN_POINT('Ctrl Pts',(12.9250540906976,0.385529703875575,4.28082461386765));
#51330=CARTESIAN_POINT('Ctrl Pts',(12.9486682068475,0.206037242841946,4.43016772408018));
#51331=CARTESIAN_POINT('Ctrl Pts',(12.9722823229973,-0.0228334776507366,
4.47641814468844));
#51332=CARTESIAN_POINT('Ctrl Pts',(12.9958964391472,-0.24623199631158,4.40849164040747));
#51333=CARTESIAN_POINT('Ctrl Pts',(13.0195105552971,-0.410619302934066,
4.24266727085754));
#51334=CARTESIAN_POINT('Ctrl Pts',(13.0431246714469,-0.476598835156983,
4.01868600055616));
#51335=CARTESIAN_POINT('Ctrl Pts',(13.0667387875968,-0.428358138764893,
3.79022650014263));
#51336=CARTESIAN_POINT('Ctrl Pts',(13.0903529037467,-0.277458432473742,
3.61204067927388));
#51337=CARTESIAN_POINT('Ctrl Pts',(13.1139670198965,-0.060063881357403,
3.52683201033335));
#51338=CARTESIAN_POINT('Ctrl Pts',(13.1375811360464,0.171725397050831,3.55502134399878));
#51339=CARTESIAN_POINT('Ctrl Pts',(13.1611952521963,0.362359488617447,3.68985291022187));
#51340=CARTESIAN_POINT('Ctrl Pts',(13.1848093683461,0.466151606229838,3.89901338554908));
#51341=CARTESIAN_POINT('Ctrl Pts',(13.208423484496,0.458227246370285,4.13237600603144));
#51342=CARTESIAN_POINT('Ctrl Pts',(13.2320376006459,0.34048553704322,4.3340137951542));
#51343=CARTESIAN_POINT('Ctrl Pts',(13.2556517167957,0.141144098528766,4.45560285308526));
#51344=CARTESIAN_POINT('Ctrl Pts',(13.2792658329456,-0.0920235057499227,
4.46800351566886));
#51345=CARTESIAN_POINT('Ctrl Pts',(13.3028799490955,-0.30313703626889,4.36824387779166));
#51346=CARTESIAN_POINT('Ctrl Pts',(13.3264940652453,-0.441601665806575,
4.18023203113149));
#51347=CARTESIAN_POINT('Ctrl Pts',(13.3501081813952,-0.47423338199515,3.94902632355453));
#51348=CARTESIAN_POINT('Ctrl Pts',(13.3737222975451,-0.393211766889608,
3.73003681238273));
#51349=CARTESIAN_POINT('Ctrl Pts',(13.3973364136949,-0.217954214568861,
3.57574585842847));
#51350=CARTESIAN_POINT('Ctrl Pts',(13.4209505298448,0.00953758252632317,
3.52313036287841));
#51351=CARTESIAN_POINT('Ctrl Pts',(13.4445646459947,0.234743631574736,3.58479999551538));
#51352=CARTESIAN_POINT('Ctrl Pts',(13.4681787621445,0.403691735186444,3.74597519957476));
#51353=CARTESIAN_POINT('Ctrl Pts',(13.4917928782944,0.475892304226004,3.96802921540861));
#51354=CARTESIAN_POINT('Ctrl Pts',(13.5154069944443,0.434041969710506,4.19774525232923));
#51355=CARTESIAN_POINT('Ctrl Pts',(13.5390211105941,0.288170455640921,4.38007026295756));
#51356=CARTESIAN_POINT('Ctrl Pts',(13.562635226744,0.0732368858249759,4.47130878927046));
#51357=CARTESIAN_POINT('Ctrl Pts',(13.5862493428939,-0.159248413505658,
4.44959488329479));
#51358=CARTESIAN_POINT('Ctrl Pts',(13.6098634590437,-0.353568721957589,
4.32013243375547));
#51359=CARTESIAN_POINT('Ctrl Pts',(13.6334775751936,-0.46315382488092,4.1139480179165));
#51360=CARTESIAN_POINT('Ctrl Pts',(13.6570916913435,-0.461740889501104,
3.88045516635315));
#51361=CARTESIAN_POINT('Ctrl Pts',(13.6807058074933,-0.349668535617837,
3.67561206636528));
#51362=CARTESIAN_POINT('Ctrl Pts',(13.7043199236432,-0.153795683012805,
3.5485107928471));
#51363=CARTESIAN_POINT('Ctrl Pts',(13.7279340397931,0.0789353756500159,
3.5296120507922));
#51364=CARTESIAN_POINT('Ctrl Pts',(13.7515481559429,0.292749022042461,3.62344505529457));
#51365=CARTESIAN_POINT('Ctrl Pts',(13.7751622720928,0.436403327377467,3.80752207362193));
#51366=CARTESIAN_POINT('Ctrl Pts',(13.7987763882427,0.475470537355291,4.03772776690975));
#51367=CARTESIAN_POINT('Ctrl Pts',(13.8223905043925,0.400587923144683,4.25889173822189));
#51368=CARTESIAN_POINT('Ctrl Pts',(13.8460046205424,0.229701624524423,4.41801050223621));
#51369=CARTESIAN_POINT('Ctrl Pts',(13.8696187366923,0.00376573255618155,
4.47695013947711));
#51370=CARTESIAN_POINT('Ctrl Pts',(13.8932328528421,-0.223072643433687,
4.42158535558109));
#51371=CARTESIAN_POINT('Ctrl Pts',(13.916846968992,-0.396450107540549,4.26518470642179));
#51372=CARTESIAN_POINT('Ctrl Pts',(13.9404610851419,-0.474815543552022,
4.04523069632808));
#51373=CARTESIAN_POINT('Ctrl Pts',(13.9640752012917,-0.439388129199652,
3.81443683499316));
#51374=CARTESIAN_POINT('Ctrl Pts',(13.9876893174416,-0.298658290955197,
3.62811447792009));
#51375=CARTESIAN_POINT('Ctrl Pts',(14.0113034335915,-0.0863529142219465,
3.53091707503438));
#51376=CARTESIAN_POINT('Ctrl Pts',(14.0349175497413,0.146647539536438,3.54613866056158));
#51377=CARTESIAN_POINT('Ctrl Pts',(14.0585316658912,0.344502889581789,3.6701312755675));
#51378=CARTESIAN_POINT('Ctrl Pts',(14.0821457820411,0.459795723937725,3.87317922671144));
#51379=CARTESIAN_POINT('Ctrl Pts',(14.1057598981909,0.464895312258427,4.10662065901627));
#51380=CARTESIAN_POINT('Ctrl Pts',(14.1293740143408,0.358579502702881,4.31450970816539));
#51381=CARTESIAN_POINT('Ctrl Pts',(14.1529881304907,0.166327619131383,4.44702431634421));
#51382=CARTESIAN_POINT('Ctrl Pts',(14.1766022466405,-0.0657858362277661,
4.47240643522367));
#51383=CARTESIAN_POINT('Ctrl Pts',(14.2002163627904,-0.282133257977474,
4.38457306332079));
#51384=CARTESIAN_POINT('Ctrl Pts',(14.2238304789403,-0.430865480427841,
4.20457407964992));
#51385=CARTESIAN_POINT('Ctrl Pts',(14.2474445950901,-0.476337791093329,
3.97554749368157));
#51386=CARTESIAN_POINT('Ctrl Pts',(14.27105871124,-0.407652434174819,3.75238112107461));
#51387=CARTESIAN_POINT('Ctrl Pts',(14.2946728273899,-0.241270333599833,
3.58855833656088));
#51388=CARTESIAN_POINT('Ctrl Pts',(14.3182869435397,-0.0170661180132474,
3.52334041087493));
#51389=CARTESIAN_POINT('Ctrl Pts',(14.3419010596896,0.211228111558234,3.57235727391142));
#51390=CARTESIAN_POINT('Ctrl Pts',(14.3655151758395,0.388900053764453,3.72386169322071));
#51391=CARTESIAN_POINT('Ctrl Pts',(14.3891292919893,0.473369390821204,3.94154458004181));
#51392=CARTESIAN_POINT('Ctrl Pts',(14.4127434081392,0.444392458083208,4.17323671518384));
#51393=CARTESIAN_POINT('Ctrl Pts',(14.4363575242891,0.308913779199362,4.3634114655727));
#51394=CARTESIAN_POINT('Ctrl Pts',(14.4599716404389,0.0994017626770733,
4.46649212840691));
#51395=CARTESIAN_POINT('Ctrl Pts',(14.4835857565888,-0.133932578240045,
4.45777470525894));
#51396=CARTESIAN_POINT('Ctrl Pts',(14.5071998727387,-0.335169044432007,
4.33934838727104));
#51397=CARTESIAN_POINT('Ctrl Pts',(14.5308139888885,-0.456079915900645,
4.13959486595487));
#51398=CARTESIAN_POINT('Ctrl Pts',(14.5544281050384,-0.467688060597361,
3.90638646324521));
#51399=CARTESIAN_POINT('Ctrl Pts',(14.5780422211883,-0.367211505836647,
3.69561319629505));
#51400=CARTESIAN_POINT('Ctrl Pts',(14.6016563373381,-0.178730157419731,
3.55778834579073));
#51401=CARTESIAN_POINT('Ctrl Pts',(14.625270453488,0.0525851174261518,3.52594259660587));
#51402=CARTESIAN_POINT('Ctrl Pts',(14.6488845696379,0.271298002813252,3.60770800421126));
#51403=CARTESIAN_POINT('Ctrl Pts',(14.6724986857877,0.424992433239313,3.78348891949988));
#51404=CARTESIAN_POINT('Ctrl Pts',(14.6961128019376,0.476834468501385,4.01115822240469));
#51405=CARTESIAN_POINT('Ctrl Pts',(14.7197269180875,0.414399804028447,4.23615337970372));
#51406=CARTESIAN_POINT('Ctrl Pts',(14.7433410342373,0.252651341641402,4.40455273546398));
#51407=CARTESIAN_POINT('Ctrl Pts',(14.7669551503872,0.0303532266559796,
4.47599821226155));
#51408=CARTESIAN_POINT('Ctrl Pts',(14.7905692665371,-0.199219250862459,
4.43336740322118));
#51409=CARTESIAN_POINT('Ctrl Pts',(14.8141833826869,-0.381047447081096,
4.28687708064914));
#51410=CARTESIAN_POINT('Ctrl Pts',(14.8377974988368,-0.471554972144783,
4.07163466550741));
#51411=CARTESIAN_POINT('Ctrl Pts',(14.8614116149867,-0.449051060899263,
3.83922451083896));
#51412=CARTESIAN_POINT('Ctrl Pts',(14.8850257311365,-0.318928946727196,
3.64534530693059));
#51413=CARTESIAN_POINT('Ctrl Pts',(14.9086398472864,-0.112373269271187,
3.53646160000302));
#51414=CARTESIAN_POINT('Ctrl Pts',(14.9322539634362,0.121113399391719,3.5386680312482));
#51415=CARTESIAN_POINT('Ctrl Pts',(14.9558680795861,0.325574495333277,3.65143602219853));
#51416=CARTESIAN_POINT('Ctrl Pts',(14.979482195736,0.452009190454857,3.84773949289016));
#51417=CARTESIAN_POINT('Ctrl Pts',(15.0030963118858,0.470117180575255,4.08053390545391));
#51418=CARTESIAN_POINT('Ctrl Pts',(15.0267104280357,0.375557372208547,4.29402641177155));
#51419=CARTESIAN_POINT('Ctrl Pts',(15.0503245441856,0.190994688421392,4.43705643304037));
#51420=CARTESIAN_POINT('Ctrl Pts',(15.0739386603355,-0.0393454023191647,
4.47533644032795));
#51421=CARTESIAN_POINT('Ctrl Pts',(15.0975527764853,-0.260245916509526,
4.39971253597763));
#51422=CARTESIAN_POINT('Ctrl Pts',(15.1211668926352,-0.418792603204267,
4.22826540530875));
#51423=CARTESIAN_POINT('Ctrl Pts',(15.1369096367351,-0.457530945318996,
4.07754232577813));
#51424=CARTESIAN_POINT('Ctrl Pts',(15.1447810087851,-0.457870370902723,
4.00205890126089));
#51425=CARTESIAN_POINT('Ctrl Pts',(12.4850729970717,-0.208850989443975,
3.53079950502365));
#51426=CARTESIAN_POINT('Ctrl Pts',(12.4929443691216,-0.131499707516366,
3.49636882573344));
#51427=CARTESIAN_POINT('Ctrl Pts',(12.5086871132215,0.0404888716816997,
3.46654221242176));
#51428=CARTESIAN_POINT('Ctrl Pts',(12.5323012293714,0.288871199237585,3.54969213591223));
#51429=CARTESIAN_POINT('Ctrl Pts',(12.5559153455212,0.467986199318594,3.74075871022993));
#51430=CARTESIAN_POINT('Ctrl Pts',(12.5795294616711,0.534963825407437,3.99395832530641));
#51431=CARTESIAN_POINT('Ctrl Pts',(12.603143577821,0.473725169098917,4.24860452170932));
#51432=CARTESIAN_POINT('Ctrl Pts',(12.6267576939708,0.298958988020687,4.4436716456386));
#51433=CARTESIAN_POINT('Ctrl Pts',(12.6503718101207,0.0525433427838623,
4.53240944903922));
#51434=CARTESIAN_POINT('Ctrl Pts',(12.6739859262706,-0.206463809544117,
4.49355177571912));
#51435=CARTESIAN_POINT('Ctrl Pts',(12.6976000424205,-0.41599087873209,4.33641091237214));
#51436=CARTESIAN_POINT('Ctrl Pts',(12.7212141585703,-0.525822648369464,
4.09864686536754));
#51437=CARTESIAN_POINT('Ctrl Pts',(12.7448282747202,-0.509637448384189,
3.8372413948162));
#51438=CARTESIAN_POINT('Ctrl Pts',(12.76844239087,-0.37131404483003,3.61484216427635));
#51439=CARTESIAN_POINT('Ctrl Pts',(12.7920565070199,-0.144002664868576,
3.48474868689319));
#51440=CARTESIAN_POINT('Ctrl Pts',(12.8156706231698,0.117819965178516,3.47813877511649));
#51441=CARTESIAN_POINT('Ctrl Pts',(12.8392847393197,0.351406216185799,3.59659653799738));
#51442=CARTESIAN_POINT('Ctrl Pts',(12.8628988554695,0.500775523187073,3.81173274911973));
#51443=CARTESIAN_POINT('Ctrl Pts',(12.8865129716194,0.530130489073712,4.07198851734671));
#51444=CARTESIAN_POINT('Ctrl Pts',(12.9101270877692,0.432435993263294,4.31499173633021));
#51445=CARTESIAN_POINT('Ctrl Pts',(12.9337412039191,0.231105201134755,4.48250499290311));
#51446=CARTESIAN_POINT('Ctrl Pts',(12.957355320069,-0.0256115611541523,
4.53438256906268));
#51447=CARTESIAN_POINT('Ctrl Pts',(12.9809694362189,-0.276190334565159,
4.45819164252092));
#51448=CARTESIAN_POINT('Ctrl Pts',(13.0045835523687,-0.460578171623014,
4.27219189922559));
#51449=CARTESIAN_POINT('Ctrl Pts',(13.0281976685186,-0.534585243620437,
4.0209594724593));
#51450=CARTESIAN_POINT('Ctrl Pts',(13.0518117846684,-0.480475240551103,
3.76470396221295));
#51451=CARTESIAN_POINT('Ctrl Pts',(13.0754259008183,-0.311216001335094,
3.5648387853972));
#51452=CARTESIAN_POINT('Ctrl Pts',(13.0990400169682,-0.0673716809183137,
3.46926302296559));
#51453=CARTESIAN_POINT('Ctrl Pts',(13.122654133118,0.19261873182715,3.50088207171981));
#51454=CARTESIAN_POINT('Ctrl Pts',(13.1462682492679,0.406446724606302,3.65211820651514));
#51455=CARTESIAN_POINT('Ctrl Pts',(13.1698823654178,0.522866930420328,3.88672663484193));
#51456=CARTESIAN_POINT('Ctrl Pts',(13.1934964815676,0.513978436505609,4.14848181366307));
#51457=CARTESIAN_POINT('Ctrl Pts',(13.2171105977175,0.381911432304553,4.37465229220773));
#51458=CARTESIAN_POINT('Ctrl Pts',(13.2407247138674,0.158316694737061,4.51103474084347));
#51459=CARTESIAN_POINT('Ctrl Pts',(13.2643388300172,-0.103219740820234,
4.52494415635039));
#51460=CARTESIAN_POINT('Ctrl Pts',(13.2879529461671,-0.340018846942428,
4.41304705047411));
#51461=CARTESIAN_POINT('Ctrl Pts',(13.311567062317,-0.495330069408668,4.20216034359148));
#51462=CARTESIAN_POINT('Ctrl Pts',(13.3351811784669,-0.531931992580964,
3.94282450306062));
#51463=CARTESIAN_POINT('Ctrl Pts',(13.3587952946167,-0.44105271077271,3.69719116838925));
#51464=CARTESIAN_POINT('Ctrl Pts',(13.3824094107666,-0.244472076510672,
3.5241280781681));
#51465=CARTESIAN_POINT('Ctrl Pts',(13.4060235269164,0.0106979927399635,
3.46511100671938));
#51466=CARTESIAN_POINT('Ctrl Pts',(13.4296376430663,0.263304213558122,3.53428380605355));
#51467=CARTESIAN_POINT('Ctrl Pts',(13.4532517592162,0.452807746647384,3.71506873327496));
#51468=CARTESIAN_POINT('Ctrl Pts',(13.476865875366,0.533792751104717,3.96413942206993));
#51469=CARTESIAN_POINT('Ctrl Pts',(13.5004799915159,0.486850606847911,4.22180434800346));
#51470=CARTESIAN_POINT('Ctrl Pts',(13.5240941076658,0.323231325528255,4.42631231788287));
#51471=CARTESIAN_POINT('Ctrl Pts',(13.5477082238157,0.0821474069231642,
4.52865157307741));
#51472=CARTESIAN_POINT('Ctrl Pts',(13.5713223399655,-0.178623709606947,
4.50429579866153));
#51473=CARTESIAN_POINT('Ctrl Pts',(13.5949364561154,-0.396586410669692,
4.35908202552279));
#51474=CARTESIAN_POINT('Ctrl Pts',(13.6185505722652,-0.519504417643299,
4.12781174527607));
#51475=CARTESIAN_POINT('Ctrl Pts',(13.6421646884151,-0.517919574482721,
3.86591049053316));
#51476=CARTESIAN_POINT('Ctrl Pts',(13.665778804565,-0.392211699884016,3.6361447201764));
#51477=CARTESIAN_POINT('Ctrl Pts',(13.6893929207148,-0.172507561089802,
3.49357940054904));
#51478=CARTESIAN_POINT('Ctrl Pts',(13.7130070368647,0.0885392156030666,
3.47238130294519));
#51479=CARTESIAN_POINT('Ctrl Pts',(13.7366211530146,0.328366952925232,3.57763069902274));
#51480=CARTESIAN_POINT('Ctrl Pts',(13.7602352691644,0.489499264105438,3.78410383833506));
#51481=CARTESIAN_POINT('Ctrl Pts',(13.7838493853143,0.533319669072828,4.04231799571659));
#51482=CARTESIAN_POINT('Ctrl Pts',(13.8074635014642,0.449326302728307,4.29039035083475));
#51483=CARTESIAN_POINT('Ctrl Pts',(13.831077617614,0.257648760022572,4.46886863686992));
#51484=CARTESIAN_POINT('Ctrl Pts',(13.8546917337639,0.00422389839726028,
4.53497929012603));
#51485=CARTESIAN_POINT('Ctrl Pts',(13.8783058499138,-0.25021324988294,4.47287843233165));
#51486=CARTESIAN_POINT('Ctrl Pts',(13.9019199660636,-0.444685051009628,
4.29744896636227));
#51487=CARTESIAN_POINT('Ctrl Pts',(13.9255340822135,-0.532584984058807,
4.05073378496132));
#51488=CARTESIAN_POINT('Ctrl Pts',(13.9491481983634,-0.492847218174075,
3.79185989881933));
#51489=CARTESIAN_POINT('Ctrl Pts',(13.9727623145132,-0.334995185577738,
3.58286823685896));
#51490=CARTESIAN_POINT('Ctrl Pts',(13.9963764306631,-0.0968592247428986,
3.47384510573062));
#51491=CARTESIAN_POINT('Ctrl Pts',(14.019990546813,0.164489723571401,3.49091865775613));
#51492=CARTESIAN_POINT('Ctrl Pts',(14.0436046629628,0.386417564563212,3.62999709733779));
#51493=CARTESIAN_POINT('Ctrl Pts',(14.0672187791127,0.515737746224078,3.85774930825782));
#51494=CARTESIAN_POINT('Ctrl Pts',(14.0908328952626,0.521457786777448,4.11959288770904));
#51495=CARTESIAN_POINT('Ctrl Pts',(14.1144470114124,0.402206838685568,4.35277519909424));
#51496=CARTESIAN_POINT('Ctrl Pts',(14.1380611275623,0.186564221804844,4.50141247822903));
#51497=CARTESIAN_POINT('Ctrl Pts',(14.1616752437122,-0.0737898095680628,
4.52988276645436));
#51498=CARTESIAN_POINT('Ctrl Pts',(14.185289359862,-0.316459599402161,4.43136296100575));
#51499=CARTESIAN_POINT('Ctrl Pts',(14.2089034760119,-0.483287643257218,
4.22946401908862));
#51500=CARTESIAN_POINT('Ctrl Pts',(14.2325175921618,-0.53429243907693,3.97257242762026));
#51501=CARTESIAN_POINT('Ctrl Pts',(14.2561317083116,-0.457250332481466,
3.72225404480531));
#51502=CARTESIAN_POINT('Ctrl Pts',(14.2797458244615,-0.270625000632592,
3.53849941363631));
#51503=CARTESIAN_POINT('Ctrl Pts',(14.3033599406114,-0.0191425034699505,
3.46534661065105));
#51504=CARTESIAN_POINT('Ctrl Pts',(14.3269740567612,0.236927627906706,3.52032721432634));
#51505=CARTESIAN_POINT('Ctrl Pts',(14.3505881729111,0.436216403922163,3.69026474025285));
#51506=CARTESIAN_POINT('Ctrl Pts',(14.374202289061,0.530962882087739,3.93443247734966));
#51507=CARTESIAN_POINT('Ctrl Pts',(14.3978164052108,0.498460409348769,4.19431392768733));
#51508=CARTESIAN_POINT('Ctrl Pts',(14.4214305213607,0.346498429557861,4.40762669256976));
#51509=CARTESIAN_POINT('Ctrl Pts',(14.4450446375106,0.111495689030631,4.52324888295055));
#51510=CARTESIAN_POINT('Ctrl Pts',(14.4686587536604,-0.150227769531968,
4.51347083601981));
#51511=CARTESIAN_POINT('Ctrl Pts',(14.4922728698103,-0.375948097339969,
4.38063592879268));
#51512=CARTESIAN_POINT('Ctrl Pts',(14.5158869859602,-0.51156984651846,4.15657897149511));
#51513=CARTESIAN_POINT('Ctrl Pts',(14.53950110211,-0.52459032076832,3.89499677367918));
#51514=CARTESIAN_POINT('Ctrl Pts',(14.5631152182599,-0.411889072794842,
3.65857933001481));
#51515=CARTESIAN_POINT('Ctrl Pts',(14.5867293344098,-0.200475741228102,
3.50398572665543));
#51516=CARTESIAN_POINT('Ctrl Pts',(14.6103434505596,0.0589829973059192,
3.46826539682992));
#51517=CARTESIAN_POINT('Ctrl Pts',(14.6339575667095,0.304306049929579,3.5599789662306));
#51518=CARTESIAN_POINT('Ctrl Pts',(14.6575716828594,0.476700039321847,3.75714663952638));
#51519=CARTESIAN_POINT('Ctrl Pts',(14.6811857990092,0.53484954579562,4.0125158112076));
#51520=CARTESIAN_POINT('Ctrl Pts',(14.7047999151591,0.464818635404008,4.26488548168423));
#51521=CARTESIAN_POINT('Ctrl Pts',(14.728414031309,0.283390703164248,4.45377350235044));
#51522=CARTESIAN_POINT('Ctrl Pts',(14.7520281474588,0.0340462163765225,
4.5339115446661));
#51523=CARTESIAN_POINT('Ctrl Pts',(14.7756422636087,-0.223457683695575,
4.48609396779546));
#51524=CARTESIAN_POINT('Ctrl Pts',(14.7992563797586,-0.427408393186059,
4.32178058932398));
#51525=CARTESIAN_POINT('Ctrl Pts',(14.8228704959084,-0.528927708313459,
4.08035024907128));
#51526=CARTESIAN_POINT('Ctrl Pts',(14.8464846120583,-0.503685810960444,
3.81966341983811));
#51527=CARTESIAN_POINT('Ctrl Pts',(14.8700987282082,-0.357732113691821,
3.6021954912391));
#51528=CARTESIAN_POINT('Ctrl Pts',(14.893712844358,-0.126045401495737,3.48006421709321));
#51529=CARTESIAN_POINT('Ctrl Pts',(14.9173269605079,0.13584891809103,3.48253909847714));
#51530=CARTESIAN_POINT('Ctrl Pts',(14.9409410766578,0.365186207068703,3.60902724630258));
#51531=CARTESIAN_POINT('Ctrl Pts',(14.9645551928076,0.507003847624586,3.82921439524653));
#51532=CARTESIAN_POINT('Ctrl Pts',(14.9881693089575,0.52731498478211,4.0903322339271));
#51533=CARTESIAN_POINT('Ctrl Pts',(15.0117834251074,0.421250356706029,4.32979975898591));
#51534=CARTESIAN_POINT('Ctrl Pts',(15.0353975412572,0.214232462415332,4.49023183125449));
#51535=CARTESIAN_POINT('Ctrl Pts',(15.0590116574071,-0.0441324441701724,
4.53316925684615));
#51536=CARTESIAN_POINT('Ctrl Pts',(15.082625773557,-0.291909288096862,4.4483444097243));
#51537=CARTESIAN_POINT('Ctrl Pts',(15.1062398897068,-0.469745893811612,
4.25603780014884));
#51538=CARTESIAN_POINT('Ctrl Pts',(15.1219826338067,-0.513197418509596,
4.08697667736293));
#51539=CARTESIAN_POINT('Ctrl Pts',(15.1298540058567,-0.513578141027115,
4.0023094018511));
#51540=CARTESIAN_POINT('Ctrl Pts',(12.4701459941433,-0.231505035597357,
3.47990537377399));
#51541=CARTESIAN_POINT('Ctrl Pts',(12.4780173661933,-0.145763467775118,
3.44174000210903));
#51542=CARTESIAN_POINT('Ctrl Pts',(12.4937601102932,0.0448806955855158,
3.40867809900361));
#51543=CARTESIAN_POINT('Ctrl Pts',(12.517374226443,0.320205029627059,3.5008472864651));
#51544=CARTESIAN_POINT('Ctrl Pts',(12.5409883425929,0.518748616038451,3.71263883318769));
#51545=CARTESIAN_POINT('Ctrl Pts',(12.5646024587428,0.592991298599855,3.99330298545039));
#51546=CARTESIAN_POINT('Ctrl Pts',(12.5882165748926,0.525110091302815,4.27557062957281));
#51547=CARTESIAN_POINT('Ctrl Pts',(12.6118306910425,0.331387039860997,4.49179666512739));
#51548=CARTESIAN_POINT('Ctrl Pts',(12.6354448071924,0.0582427139750047,
4.5901598492798));
#51549=CARTESIAN_POINT('Ctrl Pts',(12.6590589233422,-0.22885891853004,4.54708728798072));
#51550=CARTESIAN_POINT('Ctrl Pts',(12.6826730394921,-0.461113368174311,
4.37290137073994));
#51551=CARTESIAN_POINT('Ctrl Pts',(12.706287155642,-0.582858578993347,4.10934708109011));
#51552=CARTESIAN_POINT('Ctrl Pts',(12.7299012717918,-0.564917771967644,
3.8195869850214));
#51553=CARTESIAN_POINT('Ctrl Pts',(12.7535153879417,-0.411590442520908,
3.57306413195747));
#51554=CARTESIAN_POINT('Ctrl Pts',(12.7771295040916,-0.159622619673808,
3.42885942795892));
#51555=CARTESIAN_POINT('Ctrl Pts',(12.8007436202414,0.130599885139872,3.42153253970604));
#51556=CARTESIAN_POINT('Ctrl Pts',(12.8243577363913,0.38952321367407,3.55283940440193));
#51557=CARTESIAN_POINT('Ctrl Pts',(12.8479718525412,0.555094594621529,3.79131141905102));
#51558=CARTESIAN_POINT('Ctrl Pts',(12.871585968691,0.587633690752404,4.07979710469805));
#51559=CARTESIAN_POINT('Ctrl Pts',(12.8952000848409,0.479342282651013,4.34915885879276));
#51560=CARTESIAN_POINT('Ctrl Pts',(12.9188142009908,0.256173159427565,4.53484226172604));
#51561=CARTESIAN_POINT('Ctrl Pts',(12.9424283171406,-0.0283896446575681,
4.59234699343691));
#51562=CARTESIAN_POINT('Ctrl Pts',(12.9660424332905,-0.306148672818738,
4.50789164463438));
#51563=CARTESIAN_POINT('Ctrl Pts',(12.9896565494404,-0.510537040311962,
4.30171652759364));
#51564=CARTESIAN_POINT('Ctrl Pts',(13.0132706655902,-0.59257165208389,4.02323294436244));
#51565=CARTESIAN_POINT('Ctrl Pts',(13.0368847817401,-0.532592342337314,
3.73918142428326));
#51566=CARTESIAN_POINT('Ctrl Pts',(13.06049889789,-0.344973570196446,3.51763689152052));
#51567=CARTESIAN_POINT('Ctrl Pts',(13.0841130140398,-0.0746794804792245,
3.41169403559782));
#51568=CARTESIAN_POINT('Ctrl Pts',(13.1077271301897,0.213512066603468,3.44674279944083));
#51569=CARTESIAN_POINT('Ctrl Pts',(13.1313412463396,0.450533960595157,3.6143835028084));
#51570=CARTESIAN_POINT('Ctrl Pts',(13.1549553624894,0.579582254610818,3.87443988413478));
#51571=CARTESIAN_POINT('Ctrl Pts',(13.1785694786393,0.569729626640933,4.1645876212947));
#51572=CARTESIAN_POINT('Ctrl Pts',(13.2021835947892,0.423337327565886,4.41529078926125));
#51573=CARTESIAN_POINT('Ctrl Pts',(13.225797710939,0.175489290945357,4.56646662860168));
#51574=CARTESIAN_POINT('Ctrl Pts',(13.2494118270889,-0.114415975890545,
4.58188479703192));
#51575=CARTESIAN_POINT('Ctrl Pts',(13.2730259432388,-0.376900657615966,
4.45785022315656));
#51576=CARTESIAN_POINT('Ctrl Pts',(13.2966400593886,-0.54905847301076,4.22408865605146));
#51577=CARTESIAN_POINT('Ctrl Pts',(13.3202541755385,-0.589630603166779,
3.93662268256671));
#51578=CARTESIAN_POINT('Ctrl Pts',(13.3438682916884,-0.488893654655812,
3.66434552439578));
#51579=CARTESIAN_POINT('Ctrl Pts',(13.3674824078382,-0.270989938452484,
3.47251029790774));
#51580=CARTESIAN_POINT('Ctrl Pts',(13.3910965239881,0.0118584029536041,
3.40709165056035));
#51581=CARTESIAN_POINT('Ctrl Pts',(13.414710640138,0.291864795541507,3.48376761659174));
#51582=CARTESIAN_POINT('Ctrl Pts',(13.4383247562878,0.501923758108325,3.68416226697515));
#51583=CARTESIAN_POINT('Ctrl Pts',(13.4619388724377,0.591693197983429,3.96024962873126));
#51584=CARTESIAN_POINT('Ctrl Pts',(13.4855529885876,0.539659243985316,4.2458634436777));
#51585=CARTESIAN_POINT('Ctrl Pts',(13.5091671047374,0.358292195415589,4.47255437280819));
#51586=CARTESIAN_POINT('Ctrl Pts',(13.5327812208873,0.0910579280213527,
4.58599435688436));
#51587=CARTESIAN_POINT('Ctrl Pts',(13.5563953370372,-0.197999005708236,
4.55899671402827));
#51588=CARTESIAN_POINT('Ctrl Pts',(13.580009453187,-0.439604099381795,4.39803161729011));
#51589=CARTESIAN_POINT('Ctrl Pts',(13.6036235693369,-0.575855010405679,
4.14167547263565));
#51590=CARTESIAN_POINT('Ctrl Pts',(13.6272376854868,-0.574098259464336,
3.85136581471317));
#51591=CARTESIAN_POINT('Ctrl Pts',(13.6508518016366,-0.434754864150196,
3.59667737398752));
#51592=CARTESIAN_POINT('Ctrl Pts',(13.6744659177865,-0.191219439166798,
3.43864800825098));
#51593=CARTESIAN_POINT('Ctrl Pts',(13.6980800339364,0.0981430555561168,
3.41515055509818));
#51594=CARTESIAN_POINT('Ctrl Pts',(13.7216941500862,0.363984883808003,3.53181634275091));
#51595=CARTESIAN_POINT('Ctrl Pts',(13.7453082662361,0.54259520083341,3.76068560304818));
#51596=CARTESIAN_POINT('Ctrl Pts',(13.768922382386,0.591168800790367,4.04690822452342));
#51597=CARTESIAN_POINT('Ctrl Pts',(13.7925364985358,0.498064682311931,4.32188896344761));
#51598=CARTESIAN_POINT('Ctrl Pts',(13.8161506146857,0.28559589552072,4.51972677150362));
#51599=CARTESIAN_POINT('Ctrl Pts',(13.8397647308356,0.00468206423833927,
4.59300844077494));
#51600=CARTESIAN_POINT('Ctrl Pts',(13.8633788469854,-0.277353856332193,
4.52417150908221));
#51601=CARTESIAN_POINT('Ctrl Pts',(13.8869929631353,-0.492919994478707,
4.32971322630275));
#51602=CARTESIAN_POINT('Ctrl Pts',(13.9106070792852,-0.590354424565592,
4.05623687359455));
#51603=CARTESIAN_POINT('Ctrl Pts',(13.934221195435,-0.546306307148498,3.76928296264551));
#51604=CARTESIAN_POINT('Ctrl Pts',(13.9578353115849,-0.371332080200278,
3.53762199579782));
#51605=CARTESIAN_POINT('Ctrl Pts',(13.9814494277348,-0.107365535263851,
3.41677313642685));
#51606=CARTESIAN_POINT('Ctrl Pts',(14.0050635438846,0.182331907606365,3.43569865495067));
#51607=CARTESIAN_POINT('Ctrl Pts',(14.0286776600345,0.428332239544634,3.58986291910809));
#51608=CARTESIAN_POINT('Ctrl Pts',(14.0522917761844,0.571679768510432,3.8423193898042));
#51609=CARTESIAN_POINT('Ctrl Pts',(14.0759058923342,0.578020261296468,4.1325651164018));
#51610=CARTESIAN_POINT('Ctrl Pts',(14.0995200084841,0.445834174668256,4.39104069002309));
#51611=CARTESIAN_POINT('Ctrl Pts',(14.123134124634,0.206800824478305,4.55580064011384));
#51612=CARTESIAN_POINT('Ctrl Pts',(14.1467482407838,-0.0817937829083601,
4.58735909768505));
#51613=CARTESIAN_POINT('Ctrl Pts',(14.1703623569337,-0.350785940826847,
4.4781528586907));
#51614=CARTESIAN_POINT('Ctrl Pts',(14.1939764730836,-0.535709806086595,
4.25435395852733));
#51615=CARTESIAN_POINT('Ctrl Pts',(14.2175905892334,-0.59224708706053,3.96959736155895));
#51616=CARTESIAN_POINT('Ctrl Pts',(14.2412047053833,-0.506848230788112,
3.69212696853602));
#51617=CARTESIAN_POINT('Ctrl Pts',(14.2648188215332,-0.29997966766535,3.48844049071174));
#51618=CARTESIAN_POINT('Ctrl Pts',(14.288432937683,-0.0212188889266537,
3.40735281042717));
#51619=CARTESIAN_POINT('Ctrl Pts',(14.3120470538329,0.262627144255178,3.46829715474127));
#51620=CARTESIAN_POINT('Ctrl Pts',(14.3356611699828,0.483532754079872,3.65666778728498));
#51621=CARTESIAN_POINT('Ctrl Pts',(14.3592752861326,0.588556373354274,3.9273203746575));
#51622=CARTESIAN_POINT('Ctrl Pts',(14.3828894022825,0.55252836061433,4.21539114019081));
#51623=CARTESIAN_POINT('Ctrl Pts',(14.4065035184324,0.384083079916361,4.45184191956682));
#51624=CARTESIAN_POINT('Ctrl Pts',(14.4301176345822,0.123589615384189,4.58000563749418));
#51625=CARTESIAN_POINT('Ctrl Pts',(14.4537317507321,-0.166522960823891,
4.56916696678068));
#51626=CARTESIAN_POINT('Ctrl Pts',(14.477345866882,-0.416727150247931,4.42192347031433));
#51627=CARTESIAN_POINT('Ctrl Pts',(14.5009599830318,-0.567059777136274,
4.17356307703535));
#51628=CARTESIAN_POINT('Ctrl Pts',(14.5245740991817,-0.58149258093928,3.88360708411314));
#51629=CARTESIAN_POINT('Ctrl Pts',(14.5481882153316,-0.456566639753037,
3.62154546373458));
#51630=CARTESIAN_POINT('Ctrl Pts',(14.5718023314814,-0.222221325036472,
3.45018310752014));
#51631=CARTESIAN_POINT('Ctrl Pts',(14.5954164476313,0.0653808771856868,
3.41058819705396));
#51632=CARTESIAN_POINT('Ctrl Pts',(14.6190305637812,0.337314097045906,3.51224992824993));
#51633=CARTESIAN_POINT('Ctrl Pts',(14.642644679931,0.528407645404381,3.73080435955289));
#51634=CARTESIAN_POINT('Ctrl Pts',(14.6662587960809,0.592864623089856,4.0138734000105));
#51635=CARTESIAN_POINT('Ctrl Pts',(14.6898729122308,0.515237466779568,4.29361758366474));
#51636=CARTESIAN_POINT('Ctrl Pts',(14.7134870283806,0.314130064687094,4.5029942692369));
#51637=CARTESIAN_POINT('Ctrl Pts',(14.7371011445305,0.0377392060970651,
4.59182487707066));
#51638=CARTESIAN_POINT('Ctrl Pts',(14.7607152606804,-0.24769611652869,4.53882053236973));
#51639=CARTESIAN_POINT('Ctrl Pts',(14.7843293768302,-0.47376933929102,4.35668409799883));
#51640=CARTESIAN_POINT('Ctrl Pts',(14.8079434929801,-0.586300444482135,
4.08906583263515));
#51641=CARTESIAN_POINT('Ctrl Pts',(14.83155760913,-0.558320561021625,3.80010232883727));
#51642=CARTESIAN_POINT('Ctrl Pts',(14.8551717252798,-0.396535280656446,
3.55904567554761));
#51643=CARTESIAN_POINT('Ctrl Pts',(14.8787858414297,-0.139717533720287,
3.42366683418339));
#51644=CARTESIAN_POINT('Ctrl Pts',(14.9023999575795,0.150584436790342,3.42641016570609));
#51645=CARTESIAN_POINT('Ctrl Pts',(14.9260140737294,0.404797918804129,3.56661847040663));
#51646=CARTESIAN_POINT('Ctrl Pts',(14.9496281898793,0.561998504794314,3.8106892976029));
#51647=CARTESIAN_POINT('Ctrl Pts',(14.9732423060292,0.584512788988964,4.10013056240029));
#51648=CARTESIAN_POINT('Ctrl Pts',(14.996856422179,0.466943341203511,4.36557310620026));
#51649=CARTESIAN_POINT('Ctrl Pts',(15.0204705383289,0.237470236409271,4.54340722946861));
#51650=CARTESIAN_POINT('Ctrl Pts',(15.0440846544788,-0.0489194860211801,
4.59100207336435));
#51651=CARTESIAN_POINT('Ctrl Pts',(15.0676987706286,-0.323572659684198,
4.49697628347096));
#51652=CARTESIAN_POINT('Ctrl Pts',(15.0913128867785,-0.520699184418956,
4.28381019498893));
#51653=CARTESIAN_POINT('Ctrl Pts',(15.1070556308784,-0.568863891700195,
4.09641102894772));
#51654=CARTESIAN_POINT('Ctrl Pts',(15.1149270029284,-0.569285911151507,
4.00255990244131));
#51655=CARTESIAN_POINT('Ctrl Pts',(12.455218991215,-0.25415908175074,3.42901124252432));
#51656=CARTESIAN_POINT('Ctrl Pts',(12.4630903632649,-0.16002722803387,3.38711117848463));
#51657=CARTESIAN_POINT('Ctrl Pts',(12.4788331073648,0.0492725194893315,
3.35081398558546));
#51658=CARTESIAN_POINT('Ctrl Pts',(12.5024472235147,0.351538860016532,3.45200243701797));
#51659=CARTESIAN_POINT('Ctrl Pts',(12.5260613396645,0.569511032758309,3.68451895614546));
#51660=CARTESIAN_POINT('Ctrl Pts',(12.5496754558144,0.651018771792273,3.99264764559437));
#51661=CARTESIAN_POINT('Ctrl Pts',(12.5732895719643,0.576495013506714,4.3025367374363));
#51662=CARTESIAN_POINT('Ctrl Pts',(12.5969036881141,0.363815091701307,4.53992168461618));
#51663=CARTESIAN_POINT('Ctrl Pts',(12.620517804264,0.0639420851661475,4.64791024952038));
#51664=CARTESIAN_POINT('Ctrl Pts',(12.6441319204139,-0.251254027515963,
4.60062280024232));
#51665=CARTESIAN_POINT('Ctrl Pts',(12.6677460365637,-0.506235857616531,
4.40939182910775));
#51666=CARTESIAN_POINT('Ctrl Pts',(12.6913601527136,-0.639894509617229,
4.12004729681268));
#51667=CARTESIAN_POINT('Ctrl Pts',(12.7149742688635,-0.620198095551099,
3.8019325752266));
#51668=CARTESIAN_POINT('Ctrl Pts',(12.7385883850133,-0.451866840211785,
3.53128609963859));
#51669=CARTESIAN_POINT('Ctrl Pts',(12.7622025011632,-0.17524257447904,3.37297016902465));
#51670=CARTESIAN_POINT('Ctrl Pts',(12.7858166173131,0.143379805101228,3.36492630429559));
#51671=CARTESIAN_POINT('Ctrl Pts',(12.809430733463,0.42764021116234,3.50908227080648));
#51672=CARTESIAN_POINT('Ctrl Pts',(12.8330448496128,0.609413666055986,3.77089008898231));
#51673=CARTESIAN_POINT('Ctrl Pts',(12.8566589657627,0.645136892431096,4.08760569204938));
#51674=CARTESIAN_POINT('Ctrl Pts',(12.8802730819125,0.526248572038732,4.38332598125533));
#51675=CARTESIAN_POINT('Ctrl Pts',(12.9038871980624,0.281241117720374,4.58717953054897));
#51676=CARTESIAN_POINT('Ctrl Pts',(12.9275013142123,-0.0311677281609838,
4.65031141781114));
#51677=CARTESIAN_POINT('Ctrl Pts',(12.9511154303622,-0.336107011072318,
4.55759164674784));
#51678=CARTESIAN_POINT('Ctrl Pts',(12.974729546512,-0.56049590900091,4.33124115596169));
#51679=CARTESIAN_POINT('Ctrl Pts',(12.9983436626619,-0.650558060547343,
4.02550641626558));
#51680=CARTESIAN_POINT('Ctrl Pts',(13.0219577788117,-0.584709444123524,
3.71365888635357));
#51681=CARTESIAN_POINT('Ctrl Pts',(13.0455718949616,-0.378731139057797,
3.47043499764384));
#51682=CARTESIAN_POINT('Ctrl Pts',(13.0691860111115,-0.0819872800401352,
3.35412504823007));
#51683=CARTESIAN_POINT('Ctrl Pts',(13.0928001272613,0.234405401379786,3.39260352716186));
#51684=CARTESIAN_POINT('Ctrl Pts',(13.1164142434112,0.494621196584012,3.57664879910166));
#51685=CARTESIAN_POINT('Ctrl Pts',(13.1400283595611,0.636297578801308,3.86215313342763));
#51686=CARTESIAN_POINT('Ctrl Pts',(13.1636424757109,0.625480816776257,4.18069342892634));
#51687=CARTESIAN_POINT('Ctrl Pts',(13.1872565918608,0.464763222827219,4.45592928631477));
#51688=CARTESIAN_POINT('Ctrl Pts',(13.2108707080107,0.192661887153653,4.62189851635989));
#51689=CARTESIAN_POINT('Ctrl Pts',(13.2344848241605,-0.125612210960856,
4.63882543771344));
#51690=CARTESIAN_POINT('Ctrl Pts',(13.2580989403104,-0.413782468289504,
4.50265339583901));
#51691=CARTESIAN_POINT('Ctrl Pts',(13.2817130564603,-0.602786876612853,
4.24601696851145));
#51692=CARTESIAN_POINT('Ctrl Pts',(13.3053271726101,-0.647329213752593,
3.9304208620728));
#51693=CARTESIAN_POINT('Ctrl Pts',(13.32894128876,-0.536734598538914,3.6314998804023));
#51694=CARTESIAN_POINT('Ctrl Pts',(13.3525554049099,-0.297507800394296,
3.42089251764738));
#51695=CARTESIAN_POINT('Ctrl Pts',(13.3761695210598,0.0130188131672444,
3.34907229440132));
#51696=CARTESIAN_POINT('Ctrl Pts',(13.3997836372096,0.320425377524893,3.43325142712992));
#51697=CARTESIAN_POINT('Ctrl Pts',(13.4233977533595,0.551039769569266,3.65325580067535));
#51698=CARTESIAN_POINT('Ctrl Pts',(13.4470118695093,0.649593644862141,3.95635983539258));
#51699=CARTESIAN_POINT('Ctrl Pts',(13.4706259856592,0.592467881122722,4.26992253935193));
#51700=CARTESIAN_POINT('Ctrl Pts',(13.4942401018091,0.393353065302923,4.5187964277335));
#51701=CARTESIAN_POINT('Ctrl Pts',(13.5178542179589,0.0999684491195412,
4.64333714069132));
#51702=CARTESIAN_POINT('Ctrl Pts',(13.5414683341088,-0.217374301809525,
4.61369762939502));
#51703=CARTESIAN_POINT('Ctrl Pts',(13.5650824502587,-0.482621788093898,
4.43698120905743));
#51704=CARTESIAN_POINT('Ctrl Pts',(13.5886965664085,-0.632205603168059,
4.15553919999523));
#51705=CARTESIAN_POINT('Ctrl Pts',(13.6123106825584,-0.630276944445953,
3.83682113889318));
#51706=CARTESIAN_POINT('Ctrl Pts',(13.6359247987083,-0.477298028416376,
3.55721002779864));
#51707=CARTESIAN_POINT('Ctrl Pts',(13.6595389148582,-0.209931317243796,
3.38371661595291));
#51708=CARTESIAN_POINT('Ctrl Pts',(13.683153031008,0.107746895509167,3.35791980725116));
#51709=CARTESIAN_POINT('Ctrl Pts',(13.7067671471579,0.399602814690774,3.48600198647908));
#51710=CARTESIAN_POINT('Ctrl Pts',(13.7303812633077,0.59569113756138,3.73726736776131));
#51711=CARTESIAN_POINT('Ctrl Pts',(13.7539953794576,0.649017932507905,4.05149845333026));
#51712=CARTESIAN_POINT('Ctrl Pts',(13.7776094956075,0.546803061895555,4.35338757606046));
#51713=CARTESIAN_POINT('Ctrl Pts',(13.8012236117573,0.313543031018869,4.57058490613733));
#51714=CARTESIAN_POINT('Ctrl Pts',(13.8248377279072,0.00514023007941788,
4.65103759142385));
#51715=CARTESIAN_POINT('Ctrl Pts',(13.8484518440571,-0.304494462781446,
4.57546458583277));
#51716=CARTESIAN_POINT('Ctrl Pts',(13.8720659602069,-0.541154937947787,
4.36197748624323));
#51717=CARTESIAN_POINT('Ctrl Pts',(13.8956800763568,-0.648123865072376,
4.06173996222779));
#51718=CARTESIAN_POINT('Ctrl Pts',(13.9192941925067,-0.599765396122921,
3.74670602647169));
#51719=CARTESIAN_POINT('Ctrl Pts',(13.9429083086565,-0.407668974822819,
3.49237575473668));
#51720=CARTESIAN_POINT('Ctrl Pts',(13.9665224248064,-0.117871845784803,
3.35970116712309));
#51721=CARTESIAN_POINT('Ctrl Pts',(13.9901365409563,0.200174091641329,3.38047865214521));
#51722=CARTESIAN_POINT('Ctrl Pts',(14.0137506571061,0.470246914526057,3.54972874087838));
#51723=CARTESIAN_POINT('Ctrl Pts',(14.037364773256,0.627621790796785,3.82688947135059));
#51724=CARTESIAN_POINT('Ctrl Pts',(14.0609788894059,0.634582735815489,4.14553734509456));
#51725=CARTESIAN_POINT('Ctrl Pts',(14.0845930055557,0.489461510650943,4.42930618095194));
#51726=CARTESIAN_POINT('Ctrl Pts',(14.1082071217056,0.227037427151766,4.61018880199865));
#51727=CARTESIAN_POINT('Ctrl Pts',(14.1318212378555,-0.0897977562486571,
4.64483542891575));
#51728=CARTESIAN_POINT('Ctrl Pts',(14.1554353540053,-0.385112282251534,
4.52494275637564));
#51729=CARTESIAN_POINT('Ctrl Pts',(14.1790494701552,-0.588131968915973,
4.27924389796604));
#51730=CARTESIAN_POINT('Ctrl Pts',(14.2026635863051,-0.65020173504413,3.96662229549764));
#51731=CARTESIAN_POINT('Ctrl Pts',(14.2262777024549,-0.556446129094758,
3.66199989226673));
#51732=CARTESIAN_POINT('Ctrl Pts',(14.2498918186048,-0.329334334698108,
3.43838156778717));
#51733=CARTESIAN_POINT('Ctrl Pts',(14.2735059347547,-0.0232952743833569,
3.34935901020328));
#51734=CARTESIAN_POINT('Ctrl Pts',(14.2971200509045,0.28832666060365,3.41626709515619));
#51735=CARTESIAN_POINT('Ctrl Pts',(14.3207341670544,0.530849104237583,3.62307083431711));
#51736=CARTESIAN_POINT('Ctrl Pts',(14.3443482832043,0.646149864620809,3.92020827196535));
#51737=CARTESIAN_POINT('Ctrl Pts',(14.3679623993541,0.606596311879891,4.2364683526943));
#51738=CARTESIAN_POINT('Ctrl Pts',(14.391576515504,0.42166773027486,4.49605714656388));
#51739=CARTESIAN_POINT('Ctrl Pts',(14.4151906316539,0.135683541737747,4.63676239203782));
#51740=CARTESIAN_POINT('Ctrl Pts',(14.4388047478037,-0.182818152115814,
4.62486309754155));
#51741=CARTESIAN_POINT('Ctrl Pts',(14.4624188639536,-0.457506203155893,
4.46321101183598));
#51742=CARTESIAN_POINT('Ctrl Pts',(14.4860329801035,-0.622549707754089,
4.19054718257559));
#51743=CARTESIAN_POINT('Ctrl Pts',(14.5096470962533,-0.63839484111024,3.87221739454711));
#51744=CARTESIAN_POINT('Ctrl Pts',(14.5332612124032,-0.501244206711231,
3.58451159745434));
#51745=CARTESIAN_POINT('Ctrl Pts',(14.5568753285531,-0.243966908844842,
3.39638048838484));
#51746=CARTESIAN_POINT('Ctrl Pts',(14.5804894447029,0.0717787570654544,
3.35291099727801));
#51747=CARTESIAN_POINT('Ctrl Pts',(14.6041035608528,0.370322144162233,3.46452089026927));
#51748=CARTESIAN_POINT('Ctrl Pts',(14.6277176770027,0.580115251486915,3.70446207957941));
#51749=CARTESIAN_POINT('Ctrl Pts',(14.6513317931525,0.650879700384091,4.0152309888134));
#51750=CARTESIAN_POINT('Ctrl Pts',(14.6749459093024,0.565656298155129,4.32234968564526));
#51751=CARTESIAN_POINT('Ctrl Pts',(14.6985600254523,0.344869426209941,4.55221503612336));
#51752=CARTESIAN_POINT('Ctrl Pts',(14.7221741416021,0.041432195817608,4.64973820947522));
#51753=CARTESIAN_POINT('Ctrl Pts',(14.745788257752,-0.271934549361806,4.59154709694401));
#51754=CARTESIAN_POINT('Ctrl Pts',(14.7694023739019,-0.520130285395982,
4.39158760667368));
#51755=CARTESIAN_POINT('Ctrl Pts',(14.7930164900517,-0.64367318065081,4.09778141619902));
#51756=CARTESIAN_POINT('Ctrl Pts',(14.8166306062016,-0.612955311082805,
3.78054123783642));
#51757=CARTESIAN_POINT('Ctrl Pts',(14.8402447223515,-0.435338447621071,
3.51589585985611));
#51758=CARTESIAN_POINT('Ctrl Pts',(14.8638588385013,-0.153389665944836,
3.36726945127358));
#51759=CARTESIAN_POINT('Ctrl Pts',(14.8874729546512,0.165319955489652,3.37028123293502));
#51760=CARTESIAN_POINT('Ctrl Pts',(14.9110870708011,0.444409630539555,3.52420969451069));
#51761=CARTESIAN_POINT('Ctrl Pts',(14.9347011869509,0.616993161964042,3.79216419995926));
#51762=CARTESIAN_POINT('Ctrl Pts',(14.9583153031008,0.641710593195818,4.10992889087348));
#51763=CARTESIAN_POINT('Ctrl Pts',(14.9819294192507,0.512636325700993,4.40134645341462));
#51764=CARTESIAN_POINT('Ctrl Pts',(15.0055435354005,0.260708010403211,4.59658262768273));
#51765=CARTESIAN_POINT('Ctrl Pts',(15.0291576515504,-0.0537065278721878,
4.64883488988255));
#51766=CARTESIAN_POINT('Ctrl Pts',(15.0527717677003,-0.355236031271534,
4.54560815721762));
#51767=CARTESIAN_POINT('Ctrl Pts',(15.0763858838501,-0.571652475026301,
4.31158258982903));
#51768=CARTESIAN_POINT('Ctrl Pts',(15.09212862795,-0.624530364890795,4.10584538053252));
#51769=CARTESIAN_POINT('Ctrl Pts',(15.1,-0.624993681275899,4.00281040303152));
#51770=CARTESIAN_POINT('Ctrl Pts',(15.1,-0.624993681275899,4.00281040303152));
#51771=CARTESIAN_POINT('Ctrl Pts',(15.1,-0.617358358083874,4.02914127082806));
#51772=CARTESIAN_POINT('Ctrl Pts',(15.1,-0.607931963506944,4.05484759228836));
#51773=CARTESIAN_POINT('Ctrl Pts',(15.1,-0.596773861259576,4.07974656001827));
#51774=CARTESIAN_POINT('Ctrl Pts',(15.1,-0.585871522029423,4.10407480030985));
#51775=CARTESIAN_POINT('Ctrl Pts',(15.1,-0.573314772633929,4.12763281365198));
#51776=CARTESIAN_POINT('Ctrl Pts',(15.1,-0.559143639302279,4.1502040881484));
#51777=CARTESIAN_POINT('Ctrl Pts',(15.1,-0.549626121151564,4.16536325076984));
#51778=CARTESIAN_POINT('Ctrl Pts',(15.1,-0.539380106047495,4.18007635520315));
#51779=CARTESIAN_POINT('Ctrl Pts',(15.1,-0.528417753985571,4.19426420824267));
#51780=CARTESIAN_POINT('Ctrl Pts',(15.1,-0.523814643226911,4.2002217124899));
#51781=CARTESIAN_POINT('Ctrl Pts',(15.1,-0.519084627089791,4.20608691507751));
#51782=CARTESIAN_POINT('Ctrl Pts',(15.1,-0.514239086396905,4.21184190560023));
#51783=CARTESIAN_POINT('Ctrl Pts',(15.1,-0.50085552272952,4.2277374035328));
#51784=CARTESIAN_POINT('Ctrl Pts',(15.1,-0.486572803760524,4.24281789068328));
#51785=CARTESIAN_POINT('Ctrl Pts',(15.1,-0.4714177983537,4.25697008589974));
#51786=CARTESIAN_POINT('Ctrl Pts',(15.1,-0.457151696655403,4.27029219637033));
#51787=CARTESIAN_POINT('Ctrl Pts',(15.1,-0.442112042545397,4.28279146400573));
#51788=CARTESIAN_POINT('Ctrl Pts',(15.1,-0.426369607892924,4.29437520287289));
#51789=CARTESIAN_POINT('Ctrl Pts',(15.1,-0.419074661497203,4.29974303548351));
#51790=CARTESIAN_POINT('Ctrl Pts',(15.1,-0.411628924918527,4.30491398987477));
#51791=CARTESIAN_POINT('Ctrl Pts',(15.1,-0.404040271526401,4.30987739070861));
#51792=CARTESIAN_POINT('Ctrl Pts',(15.1,-0.398073367501634,4.31378007737535));
#51793=CARTESIAN_POINT('Ctrl Pts',(15.1,-0.392026704362881,4.31754881952869));
#51794=CARTESIAN_POINT('Ctrl Pts',(15.1,-0.385904261325812,4.32117966642505));
#51795=CARTESIAN_POINT('Ctrl Pts',(15.1,-0.366868686798561,4.33246850264191));
#51796=CARTESIAN_POINT('Ctrl Pts',(15.1,-0.347097727375919,4.34242824684389));
#51797=CARTESIAN_POINT('Ctrl Pts',(15.1,-0.326713262272485,4.3509180109496));
#51798=CARTESIAN_POINT('Ctrl Pts',(15.1,-0.308010762698638,4.35870726657947));
#51799=CARTESIAN_POINT('Ctrl Pts',(15.1,-0.288791261952878,4.36525839133365));
#51800=CARTESIAN_POINT('Ctrl Pts',(15.1,-0.269173508333929,4.37043259773196));
#51801=CARTESIAN_POINT('Ctrl Pts',(12.5,-0.186196943290592,3.58169363627332));
#51802=CARTESIAN_POINT('Ctrl Pts',(12.5,-0.170588484282379,3.56594316788148));
#51803=CARTESIAN_POINT('Ctrl Pts',(12.5,-0.153797667832464,3.55144458439849));
#51804=CARTESIAN_POINT('Ctrl Pts',(12.5,-0.136060690067392,3.53823162417247));
#51805=CARTESIAN_POINT('Ctrl Pts',(12.5,-0.117990710310259,3.5247705978929));
#51806=CARTESIAN_POINT('Ctrl Pts',(12.5,-0.0989385549429972,3.51264262455394));
#51807=CARTESIAN_POINT('Ctrl Pts',(12.5,-0.0790990435859813,3.5018744512649));
#51808=CARTESIAN_POINT('Ctrl Pts',(12.5,-0.0668145727052721,3.49520688224936));
#51809=CARTESIAN_POINT('Ctrl Pts',(12.5,-0.054227138249592,3.4890605701039));
#51810=CARTESIAN_POINT('Ctrl Pts',(12.5,-0.0413735013057162,3.4834433907237));
#51811=CARTESIAN_POINT('Ctrl Pts',(12.5,-0.0353493612034326,3.48081077586818));
#51812=CARTESIAN_POINT('Ctrl Pts',(12.5,-0.0292710672153644,3.47829647656688));
#51813=CARTESIAN_POINT('Ctrl Pts',(12.5,-0.0231507758853709,3.47590397706369));
#51814=CARTESIAN_POINT('Ctrl Pts',(12.5,-0.00211397253512804,3.467680423829));
#51815=CARTESIAN_POINT('Ctrl Pts',(12.5,0.0194422610390746,3.46088402724794));
#51816=CARTESIAN_POINT('Ctrl Pts',(12.5,0.0413436963816045,3.45552737346533));
#51817=CARTESIAN_POINT('Ctrl Pts',(12.5,0.0650920698750741,3.44971899548849));
#51818=CARTESIAN_POINT('Ctrl Pts',(12.5,0.089246474293393,3.44560199012534));
#51819=CARTESIAN_POINT('Ctrl Pts',(12.5,0.113633446029948,3.44311473184586));
#51820=CARTESIAN_POINT('Ctrl Pts',(12.5,0.123118497624279,3.44214733936417));
#51821=CARTESIAN_POINT('Ctrl Pts',(12.5,0.132642564327611,3.44142688205345));
#51822=CARTESIAN_POINT('Ctrl Pts',(12.5,0.142169452875131,3.44095138714122));
#51823=CARTESIAN_POINT('Ctrl Pts',(12.5,0.170359862108328,3.43954438042575));
#51824=CARTESIAN_POINT('Ctrl Pts',(12.5,0.19861482332424,3.44027367679077));
#51825=CARTESIAN_POINT('Ctrl Pts',(12.5,0.226679319731597,3.44302987267532));
#51826=CARTESIAN_POINT('Ctrl Pts',(12.5,0.254743816138955,3.44578606855986));
#51827=CARTESIAN_POINT('Ctrl Pts',(12.5,0.282619254593541,3.45056842907764));
#51828=CARTESIAN_POINT('Ctrl Pts',(12.5,0.310093463203745,3.45730861053194));
#51829=CARTESIAN_POINT('Ctrl Pts',(15.0699957084852,-1.05870731373636E-5,
4.45788944868556));
#51830=CARTESIAN_POINT('Ctrl Pts',(15.0634386537186,0.0628625045491076,
4.45782850550181));
#51831=CARTESIAN_POINT('Ctrl Pts',(15.0568815989521,0.125761012144406,4.44477074790967));
#51832=CARTESIAN_POINT('Ctrl Pts',(15.0503245441856,0.183365120595825,4.41959809737683));
#51833=CARTESIAN_POINT('Ctrl Pts',(15.0424531721356,0.252515583017112,4.38937975928409));
#51834=CARTESIAN_POINT('Ctrl Pts',(15.0345818000857,0.314036477612831,4.34170308552782));
#51835=CARTESIAN_POINT('Ctrl Pts',(15.0267104280357,0.360556892971808,4.28228266426341));
#51836=CARTESIAN_POINT('Ctrl Pts',(15.0188390559858,0.407077308330786,4.222862242999));
#51837=CARTESIAN_POINT('Ctrl Pts',(15.0109676839358,0.438597244453022,4.15169807422645));
#51838=CARTESIAN_POINT('Ctrl Pts',(15.0030963118859,0.45133921416074,4.07731692107955));
#51839=CARTESIAN_POINT('Ctrl Pts',(14.9952249398359,0.464081183868457,4.00293576793266));
#51840=CARTESIAN_POINT('Ctrl Pts',(14.9873535677859,0.458045187161657,3.92533763041141));
#51841=CARTESIAN_POINT('Ctrl Pts',(14.979482195736,0.433954739621328,3.85382131653551));
#51842=CARTESIAN_POINT('Ctrl Pts',(14.971610823686,0.409864292080999,3.78230500265962));
#51843=CARTESIAN_POINT('Ctrl Pts',(14.9637394516361,0.367719393707138,3.71687051242907));
#51844=CARTESIAN_POINT('Ctrl Pts',(14.9558680795861,0.312570095196614,3.66535860215541));
#51845=CARTESIAN_POINT('Ctrl Pts',(14.9479967075362,0.257420796686091,3.61384669188175));
#51846=CARTESIAN_POINT('Ctrl Pts',(14.9401253354862,0.189267098038905,3.57625736156498));
#51847=CARTESIAN_POINT('Ctrl Pts',(14.9322539634362,0.116275803938161,3.55709495786573));
#51848=CARTESIAN_POINT('Ctrl Pts',(14.9243825913863,0.0432845098374172,
3.53793255416647));
#51849=CARTESIAN_POINT('Ctrl Pts',(14.9165112193363,-0.0345443797168851,
3.53719707708475));
#51850=CARTESIAN_POINT('Ctrl Pts',(14.9086398472864,-0.107884770736704,
3.55497662303181));
#51851=CARTESIAN_POINT('Ctrl Pts',(14.9007684752364,-0.181225161756525,
3.57275616897888));
#51852=CARTESIAN_POINT('Ctrl Pts',(14.8928971031865,-0.250077054241862,
3.60905073795473));
#51853=CARTESIAN_POINT('Ctrl Pts',(14.8850257311365,-0.306190019513209,
3.65951122309406));
#51854=CARTESIAN_POINT('Ctrl Pts',(14.8771543590866,-0.362302984784554,
3.70997170823338));
#51855=CARTESIAN_POINT('Ctrl Pts',(14.8692829870366,-0.405677022841909,
3.77459810953617));
#51856=CARTESIAN_POINT('Ctrl Pts',(14.8614116149867,-0.431114693744839,
3.84564633596564));
#51857=CARTESIAN_POINT('Ctrl Pts',(14.8535402429367,-0.45655236464777,3.91669456239511));
#51858=CARTESIAN_POINT('Ctrl Pts',(14.8456688708867,-0.464053668396277,
3.99416461395126));
#51859=CARTESIAN_POINT('Ctrl Pts',(14.8377974988368,-0.452719732759917,
4.06877337558629));
#51860=CARTESIAN_POINT('Ctrl Pts',(14.8299261267868,-0.441385797123556,
4.14338213722132));
#51861=CARTESIAN_POINT('Ctrl Pts',(14.8220547547369,-0.411216622102327,
4.21512960893523));
#51862=CARTESIAN_POINT('Ctrl Pts',(14.8141833826869,-0.365827335221939,
4.27541839855419));
#51863=CARTESIAN_POINT('Ctrl Pts',(14.806312010637,-0.32043804834155,4.33570718817315));
#51864=CARTESIAN_POINT('Ctrl Pts',(14.798440638587,-0.259828649602004,4.38453729569717));
#51865=CARTESIAN_POINT('Ctrl Pts',(14.7905692665371,-0.191261870645823,
4.41605748429924));
#51866=CARTESIAN_POINT('Ctrl Pts',(14.7837114138531,-0.131523763221734,
4.44351912740692));
#51867=CARTESIAN_POINT('Ctrl Pts',(14.7768535611691,-0.065745536276614,
4.45784152413683));
#51868=CARTESIAN_POINT('Ctrl Pts',(14.7699957084852,8.6346448269735E-6,
4.45789857801605));
#51869=CARTESIAN_POINT('Ctrl Pts',(12.5,0.310062960217722,4.54266560670548));
#51870=CARTESIAN_POINT('Ctrl Pts',(12.50787137205,0.220600394030941,4.59378185169648));
#51871=CARTESIAN_POINT('Ctrl Pts',(12.5236141161499,0.0159878432799406,
4.65085692712531));
#51872=CARTESIAN_POINT('Ctrl Pts',(12.5472282322997,-0.294892507759568,
4.580447501361));
#51873=CARTESIAN_POINT('Ctrl Pts',(12.5708423484496,-0.535054221536356,
4.37092866956447));
#51874=CARTESIAN_POINT('Ctrl Pts',(12.5944564645995,-0.647009713430093,
4.07251155115386));
#51875=CARTESIAN_POINT('Ctrl Pts',(12.6180705807493,-0.603894380709874,
3.75671714932517));
#51876=CARTESIAN_POINT('Ctrl Pts',(12.6416846968992,-0.416056506175611,
3.49922677321964));
#51877=CARTESIAN_POINT('Ctrl Pts',(12.6652988130491,-0.128505496873939,
3.36175035317655));
#51878=CARTESIAN_POINT('Ctrl Pts',(12.6889129291989,0.189841674427298,3.37723482234205));
#51879=CARTESIAN_POINT('Ctrl Pts',(12.7125270453488,0.462692468193658,3.54196933898577));
#51880=CARTESIAN_POINT('Ctrl Pts',(12.7361411614987,0.624655556881011,3.81647407445394));
#51881=CARTESIAN_POINT('Ctrl Pts',(12.7597552776485,0.636915702199809,4.13496208375113));
#51882=CARTESIAN_POINT('Ctrl Pts',(12.7833693937984,0.496534514683115,4.42110548633398));
#51883=CARTESIAN_POINT('Ctrl Pts',(12.8069835099483,0.237155397994168,4.60632802944461));
#51884=CARTESIAN_POINT('Ctrl Pts',(12.8305976260981,-0.0790596718614395,
4.64623983861064));
#51885=CARTESIAN_POINT('Ctrl Pts',(12.854211742248,-0.376327535803878,4.5312757721487));
#51886=CARTESIAN_POINT('Ctrl Pts',(12.8778258583979,-0.583405888470749,
4.28898776831928));
#51887=CARTESIAN_POINT('Ctrl Pts',(12.9014399745477,-0.650666957548692,
3.97744183415536));
#51888=CARTESIAN_POINT('Ctrl Pts',(12.9250540906976,-0.561991161265395,
3.67130212143154));
#51889=CARTESIAN_POINT('Ctrl Pts',(12.9486682068475,-0.338630270727757,
3.44393714350224));
#51890=CARTESIAN_POINT('Ctrl Pts',(12.9722823229973,-0.0341142786054444,
3.34983650006563));
#51891=CARTESIAN_POINT('Ctrl Pts',(12.9958964391472,0.278577437919422,3.41155206540036));
#51892=CARTESIAN_POINT('Ctrl Pts',(13.0195105552971,0.524506132150044,3.61429327464512));
#51893=CARTESIAN_POINT('Ctrl Pts',(13.0431246714469,0.644733280558021,3.90947178565704));
#51894=CARTESIAN_POINT('Ctrl Pts',(13.0667387875968,0.61044561006836,4.22634601343335));
#51895=CARTESIAN_POINT('Ctrl Pts',(13.0903529037467,0.429860399609997,4.4889748434194));
#51896=CARTESIAN_POINT('Ctrl Pts',(13.1139670198965,0.146256151980267,4.63441744826062));
#51897=CARTESIAN_POINT('Ctrl Pts',(13.1375811360464,-0.172399400609521,
4.62781749523177));
#51898=CARTESIAN_POINT('Ctrl Pts',(13.1611952521963,-0.449738236712957,
4.47075670902068));
#51899=CARTESIAN_POINT('Ctrl Pts',(13.1848093683461,-0.619294173608025,
4.2008758003961));
#51900=CARTESIAN_POINT('Ctrl Pts',(13.208423484496,-0.64043195068177,3.88285360784221));
#51901=CARTESIAN_POINT('Ctrl Pts',(13.2320376006459,-0.508085752511173,
3.59290636366459));
#51902=CARTESIAN_POINT('Ctrl Pts',(13.2556517167957,-0.253973266794505,
3.40052194335125));
#51903=CARTESIAN_POINT('Ctrl Pts',(13.2792658329456,0.0610056803032868,
3.3518066124833));
#51904=CARTESIAN_POINT('Ctrl Pts',(13.3028799490955,0.361364191435218,3.45843533922715));
#51905=CARTESIAN_POINT('Ctrl Pts',(13.3264940652453,0.575119258511334,3.69485380694));
#51906=CARTESIAN_POINT('Ctrl Pts',(13.3501081813952,0.65104299168552,4.00440268404554));
#51907=CARTESIAN_POINT('Ctrl Pts',(13.3737222975451,0.570939739771795,4.31289642727099));
#51908=CARTESIAN_POINT('Ctrl Pts',(13.3973364136949,0.354006804717113,4.54640236352309));
#51909=CARTESIAN_POINT('Ctrl Pts',(13.4209505298448,0.0522336745508671,
4.6489591696652));
#51910=CARTESIAN_POINT('Ctrl Pts',(13.4445646459947,-0.26205761933777,4.59598839317277));
#51911=CARTESIAN_POINT('Ctrl Pts',(13.4681787621445,-0.513544980480383,
4.40018484937968));
#51912=CARTESIAN_POINT('Ctrl Pts',(13.4917928782944,-0.64195771209056,4.10847422061066));
#51913=CARTESIAN_POINT('Ctrl Pts',(13.5154069944443,-0.616520809113462,
3.79076698974655));
#51914=CARTESIAN_POINT('Ctrl Pts',(13.5390211105941,-0.443330402422436,
3.52320390633144));
#51915=CARTESIAN_POINT('Ctrl Pts',(13.562635226744,-0.163892778617988,3.36990832590288));
#51916=CARTESIAN_POINT('Ctrl Pts',(13.5862493428939,0.154822890495328,3.36761860145296));
#51917=CARTESIAN_POINT('Ctrl Pts',(13.6098634590437,0.43643417612693,3.51688348138565));
#51918=CARTESIAN_POINT('Ctrl Pts',(13.6334775751936,0.613450973283793,3.78193059814177));
#51919=CARTESIAN_POINT('Ctrl Pts',(13.6570916913435,0.643449974253473,4.09923956510808));
#51920=CARTESIAN_POINT('Ctrl Pts',(13.6807058074933,0.519241709620395,4.39276507945606));
#51921=CARTESIAN_POINT('Ctrl Pts',(13.7043199236432,0.270593554659618,4.59216170834183));
#51922=CARTESIAN_POINT('Ctrl Pts',(13.7279340397931,-0.0429042293685969,
4.64964266158552));
#51923=CARTESIAN_POINT('Ctrl Pts',(13.7515481559429,-0.346119716157775,
4.55143222859795));
#51924=CARTESIAN_POINT('Ctrl Pts',(13.7751622720928,-0.566385203513325,
4.32106722332061));
#51925=CARTESIAN_POINT('Ctrl Pts',(13.7987763882427,-0.650912534047929,
4.01375622291695));
#51926=CARTESIAN_POINT('Ctrl Pts',(13.8223905043925,-0.57944414457563,3.70314844792952));
#51927=CARTESIAN_POINT('Ctrl Pts',(13.8460046205424,-0.369107932149097,
3.46368321387984));
#51928=CARTESIAN_POINT('Ctrl Pts',(13.8696187366923,-0.0703124342978696,
3.35275003110641));
#51929=CARTESIAN_POINT('Ctrl Pts',(13.8932328528421,0.245333927901481,3.3969348091043));
#51930=CARTESIAN_POINT('Ctrl Pts',(13.916846968992,0.502184306426786,3.58564835824111));
#51931=CARTESIAN_POINT('Ctrl Pts',(13.9404610851419,0.638682720042094,3.87366416276737));
#51932=CARTESIAN_POINT('Ctrl Pts',(13.9640752012917,0.62211637371287,4.19195723015293));
#51933=CARTESIAN_POINT('Ctrl Pts',(13.9876893174416,0.456455507660852,4.46424641105313));
#51934=CARTESIAN_POINT('Ctrl Pts',(14.0113034335915,0.181401901656729,4.62527570776815));
#51935=CARTESIAN_POINT('Ctrl Pts',(14.0349175497413,-0.137125932879425,
4.63645332836083));
#51936=CARTESIAN_POINT('Ctrl Pts',(14.0585316658912,-0.422790583021024,
4.49510047824495));
#51937=CARTESIAN_POINT('Ctrl Pts',(14.0821457820411,-0.60713052675338,4.23509335195577));
#51938=CARTESIAN_POINT('Ctrl Pts',(14.1057598981909,-0.645967413308333,
3.91874446730605));
#51939=CARTESIAN_POINT('Ctrl Pts',(14.1293740143408,-0.529993712466286,
3.62186903671368));
#51940=CARTESIAN_POINT('Ctrl Pts',(14.1529881304907,-0.287003328966194,
3.41561532377041));
#51941=CARTESIAN_POINT('Ctrl Pts',(14.1766022466405,0.0247694002478971,
3.34941346658496));
#51942=CARTESIAN_POINT('Ctrl Pts',(14.2002163627904,0.330605970264406,3.43912920108534));
#51943=CARTESIAN_POINT('Ctrl Pts',(14.2238304789403,0.557210518047066,3.66326152695696));
#51944=CARTESIAN_POINT('Ctrl Pts',(14.2474445950901,0.650275686248857,3.96809557204375));
#51945=CARTESIAN_POINT('Ctrl Pts',(14.27105871124,0.587497759452106,4.28057573538778));
#51946=CARTESIAN_POINT('Ctrl Pts',(14.2946728273899,0.383921904832036,4.52581397056352));
#51947=CARTESIAN_POINT('Ctrl Pts',(14.3182869435397,0.088336493108731,4.64503722732482));
#51948=CARTESIAN_POINT('Ctrl Pts',(14.3419010596896,-0.22841937412829,4.6096728222354));
#51949=CARTESIAN_POINT('Ctrl Pts',(14.3655151758395,-0.490432948250941,
4.42819608115853));
#51950=CARTESIAN_POINT('Ctrl Pts',(14.3891292919893,-0.634910852255616,
4.14409916841427));
#51951=CARTESIAN_POINT('Ctrl Pts',(14.4127434081392,-0.627227950688033,
3.82546788683648));
#51952=CARTESIAN_POINT('Ctrl Pts',(14.4363575242891,-0.469225504392149,
3.54866444115539));
#51953=CARTESIAN_POINT('Ctrl Pts',(14.4599716404389,-0.198769899531221,
3.38002670405092));
#51954=CARTESIAN_POINT('Ctrl Pts',(14.4835857565888,0.11932229545683,3.35996988316441));
#51955=CARTESIAN_POINT('Ctrl Pts',(14.5071998727387,0.408818071695872,3.49330073524378));
#51956=CARTESIAN_POINT('Ctrl Pts',(14.5308139888885,0.600337751131954,3.74806559342675));
#51957=CARTESIAN_POINT('Ctrl Pts',(14.5544281050384,0.647982309355475,4.06320828594604));
#51958=CARTESIAN_POINT('Ctrl Pts',(14.5780422211883,0.540333396317157,4.36320267272319));
#51959=CARTESIAN_POINT('Ctrl Pts',(14.6016563373381,0.303189823409542,4.57615301060753));
#51960=CARTESIAN_POINT('Ctrl Pts',(14.625270453488,-0.00661530128860875,
4.65102426869959));
#51961=CARTESIAN_POINT('Ctrl Pts',(14.6488845696379,-0.314835022974042,
4.56987302880665));
#51962=CARTESIAN_POINT('Ctrl Pts',(14.6724986857877,-0.547602339746838,
4.35214775046202));
#51963=CARTESIAN_POINT('Ctrl Pts',(14.6961128019376,-0.649132943719538,
4.05002781234082));
#51964=CARTESIAN_POINT('Ctrl Pts',(14.7197269180875,-0.595094318970103,
3.73591836064326));
#51965=CARTESIAN_POINT('Ctrl Pts',(14.7433410342373,-0.398437197867616,
3.48509791236843));
#51966=CARTESIAN_POINT('Ctrl Pts',(14.7669551503872,-0.1062918289807,3.35767733339665));
#51967=CARTESIAN_POINT('Ctrl Pts',(14.7905692665371,0.211327117384507,3.38419385377023));
#51968=CARTESIAN_POINT('Ctrl Pts',(14.8141833826869,0.478300047385911,3.5582926020622));
#51969=CARTESIAN_POINT('Ctrl Pts',(14.8377974988368,0.630645044771057,3.83824960712979));
#51970=CARTESIAN_POINT('Ctrl Pts',(14.8614116149867,0.631851559871185,4.15697121131127));
#51971=CARTESIAN_POINT('Ctrl Pts',(14.8850257311365,0.481630465478622,4.4380735902585));
#51972=CARTESIAN_POINT('Ctrl Pts',(14.9086398472864,0.215983244330552,4.61418854455152));
#51973=CARTESIAN_POINT('Ctrl Pts',(14.9322539634363,-0.101425794369151,
4.64310902247508));
#51974=CARTESIAN_POINT('Ctrl Pts',(14.9558680795861,-0.394527586443172,
4.517903766532));
#51975=CARTESIAN_POINT('Ctrl Pts',(14.979482195736,-0.593077772790822,4.26857965265179));
#51976=CARTESIAN_POINT('Ctrl Pts',(15.0030963118859,-0.649493436571599,
3.95488773069898));
#51977=CARTESIAN_POINT('Ctrl Pts',(15.0267104280357,-0.550252000240565,
3.65200904506483));
#51978=CARTESIAN_POINT('Ctrl Pts',(15.0503245441856,-0.319142060764588,
3.43252503194012));
#51979=CARTESIAN_POINT('Ctrl Pts',(15.0739386603355,-0.0115409051696555,
3.34904846156061));
#51980=CARTESIAN_POINT('Ctrl Pts',(15.0975527764853,0.298810377697559,3.42155963907315));
#51981=CARTESIAN_POINT('Ctrl Pts',(15.1211668926352,0.537575400322941,3.63273573589665));
#51982=CARTESIAN_POINT('Ctrl Pts',(15.1369096367351,0.610790903144771,3.83214323401692));
#51983=CARTESIAN_POINT('Ctrl Pts',(15.1447810087851,0.621570310124627,3.93461384266089));
#51984=CARTESIAN_POINT('Ctrl Pts',(12.4850729970716,0.282426015030316,4.49429601229446));
#51985=CARTESIAN_POINT('Ctrl Pts',(12.4929443691216,0.200937545576316,4.54085609598193));
#51986=CARTESIAN_POINT('Ctrl Pts',(12.5086871132215,0.0145627935155885,
4.59284387968754));
#51987=CARTESIAN_POINT('Ctrl Pts',(12.5323012293714,-0.268607755567932,
4.52871028073968));
#51988=CARTESIAN_POINT('Ctrl Pts',(12.5559153455213,-0.487363055256749,
4.3378665608173));
#51989=CARTESIAN_POINT('Ctrl Pts',(12.5795294616711,-0.589339580973024,
4.06604835489435));
#51990=CARTESIAN_POINT('Ctrl Pts',(12.603143577821,-0.550067261575934,3.77840176074865));
#51991=CARTESIAN_POINT('Ctrl Pts',(12.6267576939709,-0.378972002925158,
3.54386236016666));
#51992=CARTESIAN_POINT('Ctrl Pts',(12.6503718101207,-0.117051373585908,
3.41863967169675));
#51993=CARTESIAN_POINT('Ctrl Pts',(12.6739859262706,0.172920453180012,3.43274395851062));
#51994=CARTESIAN_POINT('Ctrl Pts',(12.6976000424204,0.42145114619533,3.58279513857084));
#51995=CARTESIAN_POINT('Ctrl Pts',(12.7212141585703,0.568977924911017,3.83283235195095));
#51996=CARTESIAN_POINT('Ctrl Pts',(12.7448282747202,0.580145282610399,4.12293246335278));
#51997=CARTESIAN_POINT('Ctrl Pts',(12.76844239087,0.45227673827436,4.38357095065208));
#51998=CARTESIAN_POINT('Ctrl Pts',(12.7920565070199,0.216016946852954,4.55228399108678));
#51999=CARTESIAN_POINT('Ctrl Pts',(12.8156706231698,-0.0720128197761896,
4.58863832766248));
#52000=CARTESIAN_POINT('Ctrl Pts',(12.8392847393196,-0.34278420811256,4.48392139165784));
#52001=CARTESIAN_POINT('Ctrl Pts',(12.8628988554695,-0.531404976945056,
4.26322932523642));
#52002=CARTESIAN_POINT('Ctrl Pts',(12.8865129716194,-0.592670842732518,
3.97945251867098));
#52003=CARTESIAN_POINT('Ctrl Pts',(12.9101270877692,-0.51189901575794,3.70060005900794));
#52004=CARTESIAN_POINT('Ctrl Pts',(12.9337412039191,-0.308447025930223,
3.49350087944474));
#52005=CARTESIAN_POINT('Ctrl Pts',(12.957355320069,-0.0310735592390789,
3.40778774002645));
#52006=CARTESIAN_POINT('Ctrl Pts',(12.9809694362188,0.253746902286204,3.46400239130434));
#52007=CARTESIAN_POINT('Ctrl Pts',(13.0045835523687,0.477755152237737,3.64867260076509));
#52008=CARTESIAN_POINT('Ctrl Pts',(13.0281976685186,0.587266054150949,3.91754086716214));
#52009=CARTESIAN_POINT('Ctrl Pts',(13.0518117846685,0.556034558024266,4.20617103876933));
#52010=CARTESIAN_POINT('Ctrl Pts',(13.0754259008183,0.391545509324759,4.44539088570928));
#52011=CARTESIAN_POINT('Ctrl Pts',(13.0990400169682,0.133219853633759,4.57786970637232));
#52012=CARTESIAN_POINT('Ctrl Pts',(13.122654133118,-0.157032867368526,4.57185802915678));
#52013=CARTESIAN_POINT('Ctrl Pts',(13.1462682492679,-0.409651568547275,
4.42879659435664));
#52014=CARTESIAN_POINT('Ctrl Pts',(13.1698823654178,-0.564094419600429,
4.1829710707208));
#52015=CARTESIAN_POINT('Ctrl Pts',(13.1934964815676,-0.583348116144335,
3.89329525626321));
#52016=CARTESIAN_POINT('Ctrl Pts',(13.2171105977175,-0.462798375770677,
3.62919197644995));
#52017=CARTESIAN_POINT('Ctrl Pts',(13.2407247138674,-0.231335782947555,
3.45395542080054));
#52018=CARTESIAN_POINT('Ctrl Pts',(13.2643388300172,0.055568040665587,3.40958224975729));
#52019=CARTESIAN_POINT('Ctrl Pts',(13.2879529461671,0.329154596505292,3.50670680265737));
#52020=CARTESIAN_POINT('Ctrl Pts',(13.311567062317,0.523856961936024,3.72205250428141));
#52021=CARTESIAN_POINT('Ctrl Pts',(13.3351811784668,0.593013359693284,4.00401025814095));
#52022=CARTESIAN_POINT('Ctrl Pts',(13.3587952946167,0.520049977633468,4.28500692572024));
#52023=CARTESIAN_POINT('Ctrl Pts',(13.3824094107666,0.322452998189994,4.49769969952106));
#52024=CARTESIAN_POINT('Ctrl Pts',(13.4060235269164,0.0475779130258999,
4.59111527567571));
#52025=CARTESIAN_POINT('Ctrl Pts',(13.4296376430663,-0.238699550200797,
4.5428659610613));
#52026=CARTESIAN_POINT('Ctrl Pts',(13.4532517592162,-0.467771004553565,
4.36451503980497));
#52027=CARTESIAN_POINT('Ctrl Pts',(13.476865875366,-0.584737881352888,4.09880555174689));
#52028=CARTESIAN_POINT('Ctrl Pts',(13.5004799915159,-0.561568254327815,
3.80941662539381));
#52029=CARTESIAN_POINT('Ctrl Pts',(13.5240941076658,-0.403814885886516,
3.56570233148043));
#52030=CARTESIAN_POINT('Ctrl Pts',(13.5477082238157,-0.149284468950505,
3.42607049712074));
#52031=CARTESIAN_POINT('Ctrl Pts',(13.5713223399655,0.141023010189178,3.42398486344345));
#52032=CARTESIAN_POINT('Ctrl Pts',(13.5949364561154,0.39753334322815,3.55994526707815));
#52033=CARTESIAN_POINT('Ctrl Pts',(13.6185505722652,0.55877204319843,3.8013678508274));
#52034=CARTESIAN_POINT('Ctrl Pts',(13.6421646884151,0.586097133215014,4.09039401187145));
#52035=CARTESIAN_POINT('Ctrl Pts',(13.665778804565,0.47295996523623,4.35775661870721));
#52036=CARTESIAN_POINT('Ctrl Pts',(13.6893929207148,0.24647464915429,4.53938036140496));
#52037=CARTESIAN_POINT('Ctrl Pts',(13.7130070368647,-0.0390800323908759,
4.59173784568287));
#52038=CARTESIAN_POINT('Ctrl Pts',(13.7366211530146,-0.315268912124245,
4.50228123595558));
#52039=CARTESIAN_POINT('Ctrl Pts',(13.7602352691644,-0.515901402373503,
4.29244943148197));
#52040=CARTESIAN_POINT('Ctrl Pts',(13.7838493853143,-0.59289453017979,4.01253008491428));
#52041=CARTESIAN_POINT('Ctrl Pts',(13.8074635014642,-0.527796356489121,
3.72960781627073));
#52042=CARTESIAN_POINT('Ctrl Pts',(13.831077617614,-0.336208111796874,3.51148691674935));
#52043=CARTESIAN_POINT('Ctrl Pts',(13.8546917337639,-0.0640452526541193,
3.4104415783338));
#52044=CARTESIAN_POINT('Ctrl Pts',(13.8783058499138,0.223466497127862,3.45068801978614));
#52045=CARTESIAN_POINT('Ctrl Pts',(13.9019199660636,0.457422945247278,3.62258090124322));
#52046=CARTESIAN_POINT('Ctrl Pts',(13.9255340822135,0.581754800262342,3.88492489705937));
#52047=CARTESIAN_POINT('Ctrl Pts',(13.9491481983634,0.566665067602596,4.17484744237197));
#52048=CARTESIAN_POINT('Ctrl Pts',(13.9727623145132,0.415770106744681,4.42286658094793));
#52049=CARTESIAN_POINT('Ctrl Pts',(13.9963764306631,0.165232945489059,4.56954279968241));
#52050=CARTESIAN_POINT('Ctrl Pts',(14.019990546813,-0.124903441395439,4.57972412169294));
#52051=CARTESIAN_POINT('Ctrl Pts',(14.0436046629628,-0.385105849054417,
4.45097052228405));
#52052=CARTESIAN_POINT('Ctrl Pts',(14.0672187791127,-0.553014959135429,
4.21413869785145));
#52053=CARTESIAN_POINT('Ctrl Pts',(14.0908328952626,-0.58839018453545,3.92598704378684));
#52054=CARTESIAN_POINT('Ctrl Pts',(14.1144470114124,-0.482753606228458,
3.65557310990793));
#52055=CARTESIAN_POINT('Ctrl Pts',(14.1380611275623,-0.261421765577673,
3.46770347791168));
#52056=CARTESIAN_POINT('Ctrl Pts',(14.1616752437122,0.0225616210391343,
3.40740241293002));
#52057=CARTESIAN_POINT('Ctrl Pts',(14.185289359862,0.301137958114838,3.48912148496193));
#52058=CARTESIAN_POINT('Ctrl Pts',(14.2089034760119,0.507544487205137,3.69327614952086));
#52059=CARTESIAN_POINT('Ctrl Pts',(14.2325175921618,0.592314446747875,3.97093932005559));
#52060=CARTESIAN_POINT('Ctrl Pts',(14.2561317083116,0.535132125826274,4.25556708484021));
#52061=CARTESIAN_POINT('Ctrl Pts',(14.2797458244615,0.349701665714674,4.47894641865396));
#52062=CARTESIAN_POINT('Ctrl Pts',(14.3033599406114,0.0804627670229728,
4.58754290912926));
#52063=CARTESIAN_POINT('Ctrl Pts',(14.3269740567612,-0.208059593914322,
4.55533065134682));
#52064=CARTESIAN_POINT('Ctrl Pts',(14.3505881729111,-0.44671902479684,4.39002953712461));
#52065=CARTESIAN_POINT('Ctrl Pts',(14.374202289061,-0.578319131624566,4.13125512920294));
#52066=CARTESIAN_POINT('Ctrl Pts',(14.3978164052108,-0.571321032683373,
3.84102451585645));
#52067=CARTESIAN_POINT('Ctrl Pts',(14.4214305213607,-0.427401871100662,
3.58889348396707));
#52068=CARTESIAN_POINT('Ctrl Pts',(14.4450446375106,-0.181052875819672,
3.43528699049651));
#52069=CARTESIAN_POINT('Ctrl Pts',(14.4686587536604,0.108686701521778,3.41701790091169));
#52070=CARTESIAN_POINT('Ctrl Pts',(14.4922728698103,0.372378754238714,3.53846452970905));
#52071=CARTESIAN_POINT('Ctrl Pts',(14.5158869859602,0.546827646247725,3.77052134686598));
#52072=CARTESIAN_POINT('Ctrl Pts',(14.53950110211,0.59022548618159,4.05757432072539));
#52073=CARTESIAN_POINT('Ctrl Pts',(14.5631152182599,0.492171679592087,4.3308292078278));
#52074=CARTESIAN_POINT('Ctrl Pts',(14.5867293344098,0.276165503816305,4.52479857226205));
#52075=CARTESIAN_POINT('Ctrl Pts',(14.6103434505596,-0.00602565743375084,
4.59299630554951));
#52076=CARTESIAN_POINT('Ctrl Pts',(14.6339575667095,-0.286772727926288,
4.51907834617235));
#52077=CARTESIAN_POINT('Ctrl Pts',(14.6575716828594,-0.49879271786407,4.32075964763751));
#52078=CARTESIAN_POINT('Ctrl Pts',(14.6811857990092,-0.591273560669336,
4.04556866666751));
#52079=CARTESIAN_POINT('Ctrl Pts',(14.7047999151591,-0.542051578672567,
3.75945683743125));
#52080=CARTESIAN_POINT('Ctrl Pts',(14.728414031309,-0.362923162297683,3.53099285177933));
#52081=CARTESIAN_POINT('Ctrl Pts',(14.7520281474588,-0.0968176839575538,
3.41492969374656));
#52082=CARTESIAN_POINT('Ctrl Pts',(14.7756422636087,0.192490826988301,3.43908270827084));
#52083=CARTESIAN_POINT('Ctrl Pts',(14.7992563797586,0.435667569828913,3.59766345479839));
#52084=CARTESIAN_POINT('Ctrl Pts',(14.8228704959084,0.574433549780463,3.85266695881428));
#52085=CARTESIAN_POINT('Ctrl Pts',(14.8464846120583,0.575532524168,4.14297984400973));
#52086=CARTESIAN_POINT('Ctrl Pts',(14.8700987282082,0.438701136655627,4.39902663091346));
#52087=CARTESIAN_POINT('Ctrl Pts',(14.893712844358,0.196731937819222,4.55944387228049));
#52088=CARTESIAN_POINT('Ctrl Pts',(14.9173269605079,-0.0923853752310475,
4.58578657160514));
#52089=CARTESIAN_POINT('Ctrl Pts',(14.9409410766578,-0.359362027571537,
4.47174127747511));
#52090=CARTESIAN_POINT('Ctrl Pts',(14.9645551928076,-0.540214773976066,
4.24464025294543));
#52091=CARTESIAN_POINT('Ctrl Pts',(14.9881693089575,-0.59160192159185,3.95890873763601));
#52092=CARTESIAN_POINT('Ctrl Pts',(15.0117834251074,-0.501206205285789,
3.68302663884805));
#52093=CARTESIAN_POINT('Ctrl Pts',(15.0353975412572,-0.290695865081771,
3.48310596742652));
#52094=CARTESIAN_POINT('Ctrl Pts',(15.0590116574071,-0.0105122258222001,
3.40706994202017));
#52095=CARTESIAN_POINT('Ctrl Pts',(15.082625773557,0.272176412698783,3.47311795657709));
#52096=CARTESIAN_POINT('Ctrl Pts',(15.1062398897068,0.489659512974156,3.66547122397039));
#52097=CARTESIAN_POINT('Ctrl Pts',(15.1219826338067,0.5563490739778,3.84710486709154));
#52098=CARTESIAN_POINT('Ctrl Pts',(15.1298540058567,0.566167676482186,3.94044192881839));
#52099=CARTESIAN_POINT('Ctrl Pts',(12.4701459941433,0.254789069842909,4.44592641788345));
#52100=CARTESIAN_POINT('Ctrl Pts',(12.4780173661933,0.181274697121691,4.48793034026739));
#52101=CARTESIAN_POINT('Ctrl Pts',(12.4937601102932,0.0131377437512366,
4.53483083224977));
#52102=CARTESIAN_POINT('Ctrl Pts',(12.517374226443,-0.242323003376296,4.47697306011837));
#52103=CARTESIAN_POINT('Ctrl Pts',(12.5409883425929,-0.439671888977142,
4.30480445207012));
#52104=CARTESIAN_POINT('Ctrl Pts',(12.5646024587428,-0.531669448515955,
4.05958515863483));
#52105=CARTESIAN_POINT('Ctrl Pts',(12.5882165748926,-0.496240142441994,
3.80008637217214));
#52106=CARTESIAN_POINT('Ctrl Pts',(12.6118306910425,-0.341887499674706,
3.58849794711368));
#52107=CARTESIAN_POINT('Ctrl Pts',(12.6354448071924,-0.105597250297878,
3.47552899021694));
#52108=CARTESIAN_POINT('Ctrl Pts',(12.6590589233422,0.155999231932725,3.4882530946792));
#52109=CARTESIAN_POINT('Ctrl Pts',(12.6826730394921,0.380209824197002,3.62362093815591));
#52110=CARTESIAN_POINT('Ctrl Pts',(12.706287155642,0.513300292941022,3.84919062944795));
#52111=CARTESIAN_POINT('Ctrl Pts',(12.7299012717918,0.52337486302099,4.11090284295443));
#52112=CARTESIAN_POINT('Ctrl Pts',(12.7535153879417,0.408018961865605,4.34603641497018));
#52113=CARTESIAN_POINT('Ctrl Pts',(12.7771295040916,0.194878495711741,4.49823995272895));
#52114=CARTESIAN_POINT('Ctrl Pts',(12.8007436202414,-0.0649659676909401,
4.53103681671432));
#52115=CARTESIAN_POINT('Ctrl Pts',(12.8243577363913,-0.30924088042124,4.43656701116699));
#52116=CARTESIAN_POINT('Ctrl Pts',(12.8479718525412,-0.479404065419363,
4.23747088215356));
#52117=CARTESIAN_POINT('Ctrl Pts',(12.871585968691,-0.534674727916345,3.9814632031866));
#52118=CARTESIAN_POINT('Ctrl Pts',(12.8952000848409,-0.461806870250484,
3.72989799658434));
#52119=CARTESIAN_POINT('Ctrl Pts',(12.9188142009908,-0.278263781132688,
3.54306461538724));
#52120=CARTESIAN_POINT('Ctrl Pts',(12.9424283171406,-0.0280328398727138,
3.46573897998727));
#52121=CARTESIAN_POINT('Ctrl Pts',(12.9660424332905,0.228916366652986,3.51645271720832));
#52122=CARTESIAN_POINT('Ctrl Pts',(12.9896565494404,0.431004172325429,3.68305192688505));
#52123=CARTESIAN_POINT('Ctrl Pts',(13.0132706655902,0.529798827743877,3.92560994866724));
#52124=CARTESIAN_POINT('Ctrl Pts',(13.0368847817401,0.501623505980173,4.1859960641053));
#52125=CARTESIAN_POINT('Ctrl Pts',(13.06049889789,0.353230619039521,4.40180692799916));
#52126=CARTESIAN_POINT('Ctrl Pts',(13.0841130140398,0.120183555287252,4.52132196448402));
#52127=CARTESIAN_POINT('Ctrl Pts',(13.1077271301897,-0.14166633412753,4.51589856308179));
#52128=CARTESIAN_POINT('Ctrl Pts',(13.1313412463396,-0.369564900381594,
4.38683647969259));
#52129=CARTESIAN_POINT('Ctrl Pts',(13.1549553624894,-0.508894665592834,
4.16506634104549));
#52130=CARTESIAN_POINT('Ctrl Pts',(13.1785694786393,-0.5262642816069,3.9037369046842));
#52131=CARTESIAN_POINT('Ctrl Pts',(13.2021835947892,-0.417510999030181,
3.66547758923531));
#52132=CARTESIAN_POINT('Ctrl Pts',(13.225797710939,-0.208698299100604,3.50738889824983));
#52133=CARTESIAN_POINT('Ctrl Pts',(13.2494118270889,0.0501304010278875,
3.46735788703128));
#52134=CARTESIAN_POINT('Ctrl Pts',(13.2730259432388,0.296945001575366,3.55497826608759));
#52135=CARTESIAN_POINT('Ctrl Pts',(13.2966400593886,0.472594665360713,3.74925120162283));
#52136=CARTESIAN_POINT('Ctrl Pts',(13.3202541755385,0.534983727701048,4.00361783223636));
#52137=CARTESIAN_POINT('Ctrl Pts',(13.3438682916884,0.469160215495142,4.25711742416948));
#52138=CARTESIAN_POINT('Ctrl Pts',(13.3674824078382,0.290899191662876,4.44899703551904));
#52139=CARTESIAN_POINT('Ctrl Pts',(13.3910965239881,0.0429221515009326,
4.53327138168622));
#52140=CARTESIAN_POINT('Ctrl Pts',(13.414710640138,-0.215341481063824,4.48974352894983));
#52141=CARTESIAN_POINT('Ctrl Pts',(13.4383247562878,-0.421997028626747,
4.32884523023027));
#52142=CARTESIAN_POINT('Ctrl Pts',(13.4619388724377,-0.527518050615216,
4.08913688288313));
#52143=CARTESIAN_POINT('Ctrl Pts',(13.4855529885876,-0.506615699542168,
3.82806626104107));
#52144=CARTESIAN_POINT('Ctrl Pts',(13.5091671047374,-0.364299369350597,
3.60820075662942));
#52145=CARTESIAN_POINT('Ctrl Pts',(13.5327812208873,-0.134676159283021,
3.48223266833859));
#52146=CARTESIAN_POINT('Ctrl Pts',(13.5563953370372,0.127223129883027,3.48035112543394));
#52147=CARTESIAN_POINT('Ctrl Pts',(13.580009453187,0.35863251032937,3.60300705277064));
#52148=CARTESIAN_POINT('Ctrl Pts',(13.6036235693369,0.504093113113068,3.82080510351303));
#52149=CARTESIAN_POINT('Ctrl Pts',(13.6272376854868,0.528744292176554,4.08154845863482));
#52150=CARTESIAN_POINT('Ctrl Pts',(13.6508518016366,0.426678220852065,4.32274815795836));
#52151=CARTESIAN_POINT('Ctrl Pts',(13.6744659177865,0.222355743648963,4.48659901446809));
#52152=CARTESIAN_POINT('Ctrl Pts',(13.6980800339364,-0.0352558354131549,
4.53383302978021));
#52153=CARTESIAN_POINT('Ctrl Pts',(13.7216941500862,-0.284418108090716,
4.45313024331322));
#52154=CARTESIAN_POINT('Ctrl Pts',(13.7453082662361,-0.465417601233682,
4.26383163964332));
#52155=CARTESIAN_POINT('Ctrl Pts',(13.768922382386,-0.534876526311652,4.01130394691162));
#52156=CARTESIAN_POINT('Ctrl Pts',(13.7925364985358,-0.476148568402614,
3.75606718461195));
#52157=CARTESIAN_POINT('Ctrl Pts',(13.8161506146857,-0.303308291444651,
3.55929061961886));
#52158=CARTESIAN_POINT('Ctrl Pts',(13.8397647308356,-0.0577780710103693,
3.46813312556118));
#52159=CARTESIAN_POINT('Ctrl Pts',(13.8633788469854,0.201599066354243,3.50444123046797));
#52160=CARTESIAN_POINT('Ctrl Pts',(13.8869929631353,0.412661584067771,3.65951344424533));
#52161=CARTESIAN_POINT('Ctrl Pts',(13.9106070792852,0.52482688048259,3.89618563135138));
#52162=CARTESIAN_POINT('Ctrl Pts',(13.934221195435,0.511213761492322,4.157737654591));
#52163=CARTESIAN_POINT('Ctrl Pts',(13.9578353115849,0.375084705828511,4.38148675084272));
#52164=CARTESIAN_POINT('Ctrl Pts',(13.9814494277348,0.149063989321389,4.51380989159668));
#52165=CARTESIAN_POINT('Ctrl Pts',(14.0050635438846,-0.112680949911453,
4.52299491502504));
#52166=CARTESIAN_POINT('Ctrl Pts',(14.0286776600345,-0.347421115087809,
4.40684056632315));
#52167=CARTESIAN_POINT('Ctrl Pts',(14.0522917761844,-0.498899391517477,
4.19318404374712));
#52168=CARTESIAN_POINT('Ctrl Pts',(14.0759058923342,-0.530812955762567,
3.93322962026762));
#52169=CARTESIAN_POINT('Ctrl Pts',(14.0995200084841,-0.435513499990629,
3.68927718310219));
#52170=CARTESIAN_POINT('Ctrl Pts',(14.123134124634,-0.235840202189154,3.51979163205294));
#52171=CARTESIAN_POINT('Ctrl Pts',(14.1467482407838,0.020353841830372,3.46539135927508));
#52172=CARTESIAN_POINT('Ctrl Pts',(14.1703623569337,0.271669945965271,3.53911376883853));
#52173=CARTESIAN_POINT('Ctrl Pts',(14.1939764730836,0.457878456363209,3.72329077208477));
#52174=CARTESIAN_POINT('Ctrl Pts',(14.2175905892334,0.534353207246894,3.97378306806742));
#52175=CARTESIAN_POINT('Ctrl Pts',(14.2412047053833,0.482766492200443,4.23055843429265));
#52176=CARTESIAN_POINT('Ctrl Pts',(14.2648188215332,0.315481426597312,4.4320788667444));
#52177=CARTESIAN_POINT('Ctrl Pts',(14.288432937683,0.0725890409372144,4.53004859093371));
#52178=CARTESIAN_POINT('Ctrl Pts',(14.3120470538329,-0.187699813700353,
4.50098848045824));
#52179=CARTESIAN_POINT('Ctrl Pts',(14.3356611699828,-0.40300510134274,4.35186299309067));
#52180=CARTESIAN_POINT('Ctrl Pts',(14.3592752861326,-0.521727410993515,
4.11841108999162));
#52181=CARTESIAN_POINT('Ctrl Pts',(14.3828894022825,-0.515414114678713,
3.85658114487643));
#52182=CARTESIAN_POINT('Ctrl Pts',(14.4065035184324,-0.385578237809175,
3.62912252677875));
#52183=CARTESIAN_POINT('Ctrl Pts',(14.4301176345822,-0.163335852108122,
3.49054727694211));
#52184=CARTESIAN_POINT('Ctrl Pts',(14.4537317507321,0.0980511075867261,
3.47406591865897));
#52185=CARTESIAN_POINT('Ctrl Pts',(14.477345866882,0.335939436781555,3.58362832417432));
#52186=CARTESIAN_POINT('Ctrl Pts',(14.5009599830318,0.493317541363497,3.79297710030521));
#52187=CARTESIAN_POINT('Ctrl Pts',(14.5245740991817,0.532468663007706,4.05194035550473));
#52188=CARTESIAN_POINT('Ctrl Pts',(14.5481882153316,0.444009962867018,4.2984557429324));
#52189=CARTESIAN_POINT('Ctrl Pts',(14.5718023314814,0.249141184223067,4.47344413391656));
#52190=CARTESIAN_POINT('Ctrl Pts',(14.5954164476313,-0.00543601357889273,
4.53496834239941));
#52191=CARTESIAN_POINT('Ctrl Pts',(14.6190305637812,-0.258710432878536,
4.46828366353805));
#52192=CARTESIAN_POINT('Ctrl Pts',(14.642644679931,-0.449983095981302,4.28937154481299));
#52193=CARTESIAN_POINT('Ctrl Pts',(14.6662587960809,-0.533414177619135,
4.0411095209942));
#52194=CARTESIAN_POINT('Ctrl Pts',(14.6898729122308,-0.489008838375032,
3.78299531421925));
#52195=CARTESIAN_POINT('Ctrl Pts',(14.7134870283806,-0.327409126727749,
3.57688779119022));
#52196=CARTESIAN_POINT('Ctrl Pts',(14.7371011445305,-0.0873435389344073,
3.47218205409647));
#52197=CARTESIAN_POINT('Ctrl Pts',(14.7607152606804,0.173654536592096,3.49397156277145));
#52198=CARTESIAN_POINT('Ctrl Pts',(14.7843293768302,0.393035092271916,3.63703430753458));
#52199=CARTESIAN_POINT('Ctrl Pts',(14.8079434929801,0.518222054789869,3.86708431049878));
#52200=CARTESIAN_POINT('Ctrl Pts',(14.8315576091299,0.519213488464815,4.12898847670818));
#52201=CARTESIAN_POINT('Ctrl Pts',(14.8551717252798,0.395771807832633,4.35997967156842));
#52202=CARTESIAN_POINT('Ctrl Pts',(14.8787858414297,0.177480631307892,4.50469920000947));
#52203=CARTESIAN_POINT('Ctrl Pts',(14.9023999575796,-0.0833449560929437,
4.52846412073519));
#52204=CARTESIAN_POINT('Ctrl Pts',(14.9260140737294,-0.324196468699902,
4.42557878841823));
#52205=CARTESIAN_POINT('Ctrl Pts',(14.9496281898793,-0.487351775161311,
4.22070085323907));
#52206=CARTESIAN_POINT('Ctrl Pts',(14.9732423060292,-0.533710406612102,
3.96292974457304));
#52207=CARTESIAN_POINT('Ctrl Pts',(14.996856422179,-0.452160410331013,3.71404423263127));
#52208=CARTESIAN_POINT('Ctrl Pts',(15.0204705383289,-0.262249669398955,
3.53368690291293));
#52209=CARTESIAN_POINT('Ctrl Pts',(15.0440846544788,-0.0094835464747447,
3.46509142247974));
#52210=CARTESIAN_POINT('Ctrl Pts',(15.0676987706286,0.245542447700007,3.52467627408104));
#52211=CARTESIAN_POINT('Ctrl Pts',(15.0913128867785,0.441743625625371,3.69820671204414));
#52212=CARTESIAN_POINT('Ctrl Pts',(15.1070556308784,0.501907244810829,3.86206650016617));
#52213=CARTESIAN_POINT('Ctrl Pts',(15.1149270029284,0.510765042839744,3.94627001497588));
#52214=CARTESIAN_POINT('Ctrl Pts',(12.4552189912149,0.227152124655503,4.39755682347243));
#52215=CARTESIAN_POINT('Ctrl Pts',(12.4630903632649,0.161611848667067,4.43500458455284));
#52216=CARTESIAN_POINT('Ctrl Pts',(12.4788331073648,0.0117126939868845,
4.476817784812));
#52217=CARTESIAN_POINT('Ctrl Pts',(12.5024472235147,-0.216038251184659,
4.42523583949706));
#52218=CARTESIAN_POINT('Ctrl Pts',(12.5260613396645,-0.391980722697534,
4.27174234332294));
#52219=CARTESIAN_POINT('Ctrl Pts',(12.5496754558144,-0.473999316058885,
4.05312196237532));
#52220=CARTESIAN_POINT('Ctrl Pts',(12.5732895719643,-0.442413023308054,
3.82177098359562));
#52221=CARTESIAN_POINT('Ctrl Pts',(12.5969036881141,-0.304802996424253,
3.6331335340607));
#52222=CARTESIAN_POINT('Ctrl Pts',(12.620517804264,-0.0941431270098475,
3.53241830873714));
#52223=CARTESIAN_POINT('Ctrl Pts',(12.6441319204139,0.139078010685439,3.54376223084778));
#52224=CARTESIAN_POINT('Ctrl Pts',(12.6677460365637,0.338968502198674,3.66444673774097));
#52225=CARTESIAN_POINT('Ctrl Pts',(12.6913601527136,0.457622660971028,3.86554890694496));
#52226=CARTESIAN_POINT('Ctrl Pts',(12.7149742688635,0.46660444343158,4.09887322255608));
#52227=CARTESIAN_POINT('Ctrl Pts',(12.7385883850133,0.36376118545685,4.30850187928827));
#52228=CARTESIAN_POINT('Ctrl Pts',(12.7622025011632,0.173740044570527,4.44419591437112));
#52229=CARTESIAN_POINT('Ctrl Pts',(12.7858166173131,-0.0579191156056905,
4.47343530576616));
#52230=CARTESIAN_POINT('Ctrl Pts',(12.809430733463,-0.275697552729921,4.38921263067613));
#52231=CARTESIAN_POINT('Ctrl Pts',(12.8330448496128,-0.42740315389367,4.2117124390707));
#52232=CARTESIAN_POINT('Ctrl Pts',(12.8566589657627,-0.476678613100171,
3.98347388770222));
#52233=CARTESIAN_POINT('Ctrl Pts',(12.8802730819125,-0.411714724743029,
3.75919593416074));
#52234=CARTESIAN_POINT('Ctrl Pts',(12.9038871980624,-0.248080536335154,
3.59262835132974));
#52235=CARTESIAN_POINT('Ctrl Pts',(12.9275013142123,-0.0249921205063485,
3.52369021994808));
#52236=CARTESIAN_POINT('Ctrl Pts',(12.9511154303621,0.204085831019768,3.5689030431123));
#52237=CARTESIAN_POINT('Ctrl Pts',(12.974729546512,0.384253192413122,3.71743125300502));
#52238=CARTESIAN_POINT('Ctrl Pts',(12.9983436626619,0.472331601336806,3.93367903017235));
#52239=CARTESIAN_POINT('Ctrl Pts',(13.0219577788117,0.44721245393608,4.16582108944128));
#52240=CARTESIAN_POINT('Ctrl Pts',(13.0455718949616,0.314915728754283,4.35822297028905));
#52241=CARTESIAN_POINT('Ctrl Pts',(13.0691860111115,0.107147256940744,4.46477422259573));
#52242=CARTESIAN_POINT('Ctrl Pts',(13.0928001272613,-0.126299800886535,
4.4599390970068));
#52243=CARTESIAN_POINT('Ctrl Pts',(13.1164142434112,-0.329478232215912,
4.34487636502855));
#52244=CARTESIAN_POINT('Ctrl Pts',(13.1400283595611,-0.453694911585238,
4.14716161137019));
#52245=CARTESIAN_POINT('Ctrl Pts',(13.1636424757109,-0.469180447069464,
3.9141785531052));
#52246=CARTESIAN_POINT('Ctrl Pts',(13.1872565918608,-0.372223622289685,
3.70176320202068));
#52247=CARTESIAN_POINT('Ctrl Pts',(13.2108707080107,-0.186060815253654,
3.56082237569912));
#52248=CARTESIAN_POINT('Ctrl Pts',(13.2344848241605,0.0446927613901878,
3.52513352430527));
#52249=CARTESIAN_POINT('Ctrl Pts',(13.2580989403104,0.26473540664544,3.60324972951781));
#52250=CARTESIAN_POINT('Ctrl Pts',(13.2817130564603,0.421332368785403,3.77644989896424));
#52251=CARTESIAN_POINT('Ctrl Pts',(13.3053271726101,0.476954095708811,4.00322540633176));
#52252=CARTESIAN_POINT('Ctrl Pts',(13.32894128876,0.418270453356816,4.22922792261873));
#52253=CARTESIAN_POINT('Ctrl Pts',(13.3525554049099,0.259345385135757,4.40029437151701));
#52254=CARTESIAN_POINT('Ctrl Pts',(13.3761695210597,0.0382663899759653,
4.47542748769673));
#52255=CARTESIAN_POINT('Ctrl Pts',(13.3997836372096,-0.19198341192685,4.43662109683837));
#52256=CARTESIAN_POINT('Ctrl Pts',(13.4233977533595,-0.376223052699929,
4.29317542065556));
#52257=CARTESIAN_POINT('Ctrl Pts',(13.4470118695093,-0.470298219877544,
4.07946821401937));
#52258=CARTESIAN_POINT('Ctrl Pts',(13.4706259856592,-0.451663144756522,
3.84671589668833));
#52259=CARTESIAN_POINT('Ctrl Pts',(13.4942401018091,-0.324783852814677,
3.65069918177841));
#52260=CARTESIAN_POINT('Ctrl Pts',(13.5178542179589,-0.120067849615538,
3.53839483955645));
#52261=CARTESIAN_POINT('Ctrl Pts',(13.5414683341088,0.113423249576877,3.53671738742444));
#52262=CARTESIAN_POINT('Ctrl Pts',(13.5650824502587,0.319731677430589,3.64606883846313));
#52263=CARTESIAN_POINT('Ctrl Pts',(13.5886965664085,0.449414183027706,3.84024235619866));
#52264=CARTESIAN_POINT('Ctrl Pts',(13.6123106825584,0.471391451138094,4.07270290539818));
#52265=CARTESIAN_POINT('Ctrl Pts',(13.6359247987083,0.380396476467901,4.28773969720951));
#52266=CARTESIAN_POINT('Ctrl Pts',(13.6595389148581,0.198236838143636,4.43381766753122));
#52267=CARTESIAN_POINT('Ctrl Pts',(13.683153031008,-0.0314316384354341,
4.47592821387755));
#52268=CARTESIAN_POINT('Ctrl Pts',(13.7067671471579,-0.253567304057185,
4.40397925067086));
#52269=CARTESIAN_POINT('Ctrl Pts',(13.7303812633077,-0.414933800093862,
4.23521384780468));
#52270=CARTESIAN_POINT('Ctrl Pts',(13.7539953794576,-0.476858522443512,
4.01007780890896));
#52271=CARTESIAN_POINT('Ctrl Pts',(13.7776094956075,-0.424500780316106,
3.78252655295316));
#52272=CARTESIAN_POINT('Ctrl Pts',(13.8012236117573,-0.270408471092428,
3.60709432248837));
#52273=CARTESIAN_POINT('Ctrl Pts',(13.8248377279072,-0.0515108893666192,
3.52582467278856));
#52274=CARTESIAN_POINT('Ctrl Pts',(13.8484518440571,0.179731635580624,3.55819444114981));
#52275=CARTESIAN_POINT('Ctrl Pts',(13.8720659602069,0.367900222888263,3.69644598724744));
#52276=CARTESIAN_POINT('Ctrl Pts',(13.8956800763568,0.467898960702838,3.90744636564338));
#52277=CARTESIAN_POINT('Ctrl Pts',(13.9192941925067,0.455762455382048,4.14062786681004));
#52278=CARTESIAN_POINT('Ctrl Pts',(13.9429083086565,0.33439930491234,4.34010692073752));
#52279=CARTESIAN_POINT('Ctrl Pts',(13.9665224248064,0.132895033153719,4.45807698351094));
#52280=CARTESIAN_POINT('Ctrl Pts',(13.9901365409563,-0.100458458427467,
4.46626570835715));
#52281=CARTESIAN_POINT('Ctrl Pts',(14.0137506571061,-0.309736381121202,
4.36271061036225));
#52282=CARTESIAN_POINT('Ctrl Pts',(14.037364773256,-0.444783823899526,4.1722293896428));
#52283=CARTESIAN_POINT('Ctrl Pts',(14.0609788894059,-0.473235726989685,
3.94047219674841));
#52284=CARTESIAN_POINT('Ctrl Pts',(14.0845930055557,-0.388273393752801,
3.72298125629644));
#52285=CARTESIAN_POINT('Ctrl Pts',(14.1082071217056,-0.210258638800633,
3.5718797861942));
#52286=CARTESIAN_POINT('Ctrl Pts',(14.1318212378555,0.0181460626216094,
3.52338030562014));
#52287=CARTESIAN_POINT('Ctrl Pts',(14.1554353540053,0.242201933815703,3.58910605271512));
#52288=CARTESIAN_POINT('Ctrl Pts',(14.1790494701552,0.40821242552128,3.75330539464867));
#52289=CARTESIAN_POINT('Ctrl Pts',(14.2026635863051,0.476391967745912,3.97662681607925));
#52290=CARTESIAN_POINT('Ctrl Pts',(14.2262777024549,0.430400858574612,4.20554978374509));
#52291=CARTESIAN_POINT('Ctrl Pts',(14.2498918186048,0.28126118747995,4.38521131483484));
#52292=CARTESIAN_POINT('Ctrl Pts',(14.2735059347547,0.0647153148514563,
4.47255427273816));
#52293=CARTESIAN_POINT('Ctrl Pts',(14.2971200509045,-0.167340033486385,
4.44664630956965));
#52294=CARTESIAN_POINT('Ctrl Pts',(14.3207341670544,-0.359291177888639,
4.31369644905674));
#52295=CARTESIAN_POINT('Ctrl Pts',(14.3443482832043,-0.465135690362464,
4.10556705078029));
#52296=CARTESIAN_POINT('Ctrl Pts',(14.3679623993541,-0.459507196674052,
3.87213777389641));
#52297=CARTESIAN_POINT('Ctrl Pts',(14.391576515504,-0.343754604517688,3.66935156959044));
#52298=CARTESIAN_POINT('Ctrl Pts',(14.4151906316539,-0.145618828396573,
3.5458075633877));
#52299=CARTESIAN_POINT('Ctrl Pts',(14.4388047478037,0.0874155136516737,
3.53111393640625));
#52300=CARTESIAN_POINT('Ctrl Pts',(14.4624188639536,0.299500119324396,3.6287921186396));
#52301=CARTESIAN_POINT('Ctrl Pts',(14.4860329801035,0.439807436479269,3.81543285374444));
#52302=CARTESIAN_POINT('Ctrl Pts',(14.5096470962533,0.474711839833821,4.04630639028407));
#52303=CARTESIAN_POINT('Ctrl Pts',(14.5332612124032,0.395848246141948,4.26608227803701));
#52304=CARTESIAN_POINT('Ctrl Pts',(14.5568753285531,0.22211686462983,4.42208969557108));
#52305=CARTESIAN_POINT('Ctrl Pts',(14.5804894447029,-0.00484636972403486,
4.47694037924932));
#52306=CARTESIAN_POINT('Ctrl Pts',(14.6041035608528,-0.230648137830783,
4.41748898090375));
#52307=CARTESIAN_POINT('Ctrl Pts',(14.6277176770027,-0.401173474098533,
4.25798344198848));
#52308=CARTESIAN_POINT('Ctrl Pts',(14.6513317931525,-0.475554794568933,
4.03665037532088));
#52309=CARTESIAN_POINT('Ctrl Pts',(14.6749459093024,-0.435966098077497,
3.80653379100725));
#52310=CARTESIAN_POINT('Ctrl Pts',(14.6985600254523,-0.291895091157815,
3.62278273060111));
#52311=CARTESIAN_POINT('Ctrl Pts',(14.7221741416021,-0.077869393911261,
3.52943441444639));
#52312=CARTESIAN_POINT('Ctrl Pts',(14.745788257752,0.15481824619589,3.54886041727207));
#52313=CARTESIAN_POINT('Ctrl Pts',(14.7694023739019,0.350402614714918,3.67640516027076));
#52314=CARTESIAN_POINT('Ctrl Pts',(14.7930164900517,0.462010559799276,3.88150166218328));
#52315=CARTESIAN_POINT('Ctrl Pts',(14.8166306062016,0.46289445276163,4.11499710940664));
#52316=CARTESIAN_POINT('Ctrl Pts',(14.8402447223515,0.352842479009638,4.32093271222338));
#52317=CARTESIAN_POINT('Ctrl Pts',(14.8638588385013,0.158229324796562,4.44995452773844));
#52318=CARTESIAN_POINT('Ctrl Pts',(14.8874729546512,-0.07430453695484,4.47114166986524));
#52319=CARTESIAN_POINT('Ctrl Pts',(14.9110870708011,-0.289030909828268,
4.37941629936134));
#52320=CARTESIAN_POINT('Ctrl Pts',(14.9347011869509,-0.434488776346555,
4.1967614535327));
#52321=CARTESIAN_POINT('Ctrl Pts',(14.9583153031008,-0.475818891632353,
3.96695075151007));
#52322=CARTESIAN_POINT('Ctrl Pts',(14.9819294192507,-0.403114615376237,
3.74506182641449));
#52323=CARTESIAN_POINT('Ctrl Pts',(15.0055435354005,-0.233803473716137,
3.58426783839933));
#52324=CARTESIAN_POINT('Ctrl Pts',(15.0291576515504,-0.00845486712728951,
3.5231129029393));
#52325=CARTESIAN_POINT('Ctrl Pts',(15.0527717677003,0.218908482701231,3.57623459158499));
#52326=CARTESIAN_POINT('Ctrl Pts',(15.0763858838501,0.393827738276586,3.73094220011788));
#52327=CARTESIAN_POINT('Ctrl Pts',(15.09212862795,0.447465415643859,3.87702813324079));
#52328=CARTESIAN_POINT('Ctrl Pts',(15.1,0.455362409197302,3.95209810113337));
#52329=CARTESIAN_POINT('',(15.1,0.455362409197302,3.95209810113338));
#52330=CARTESIAN_POINT('Ctrl Pts',(15.1,0.455362409197302,3.95209810113337));
#52331=CARTESIAN_POINT('Ctrl Pts',(15.1,0.461198486074795,3.93070554260298));
#52332=CARTESIAN_POINT('Ctrl Pts',(15.1,0.46535922191849,3.9089149747703));
#52333=CARTESIAN_POINT('Ctrl Pts',(15.1,0.467933495509747,3.88694781877637));
#52334=CARTESIAN_POINT('Ctrl Pts',(15.1,0.470556099470815,3.86456824322593));
#52335=CARTESIAN_POINT('Ctrl Pts',(15.1,0.471533159003394,3.84200460508655));
#52336=CARTESIAN_POINT('Ctrl Pts',(15.1,0.470938919222204,3.8194389967166));
#52337=CARTESIAN_POINT('Ctrl Pts',(15.1,0.470570970565677,3.80546654730098));
#52338=CARTESIAN_POINT('Ctrl Pts',(15.1,0.469600118414825,3.7914923521806));
#52339=CARTESIAN_POINT('Ctrl Pts',(15.1,0.468037922355437,3.77755218535593));
#52340=CARTESIAN_POINT('Ctrl Pts',(15.1,0.467305764617198,3.77101881782393));
#52341=CARTESIAN_POINT('Ctrl Pts',(15.1,0.466444065557791,3.76449770946228));
#52342=CARTESIAN_POINT('Ctrl Pts',(15.1,0.465455885979624,3.7580011302485));
#52343=CARTESIAN_POINT('Ctrl Pts',(15.1,0.462059294618766,3.73567095330476));
#52344=CARTESIAN_POINT('Ctrl Pts',(15.1,0.45716703427379,3.71360451488159));
#52345=CARTESIAN_POINT('Ctrl Pts',(15.1,0.450855318277529,3.69195899424001));
#52346=CARTESIAN_POINT('Ctrl Pts',(15.1,0.444011336009419,3.66848810937402));
#52347=CARTESIAN_POINT('Ctrl Pts',(15.1,0.435499564516811,3.64551127788848));
#52348=CARTESIAN_POINT('Ctrl Pts',(15.1,0.425460105602329,3.62314791088594));
#52349=CARTESIAN_POINT('Ctrl Pts',(15.1,0.421555366121865,3.61444992000866));
#52350=CARTESIAN_POINT('Ctrl Pts',(15.1,0.417417266816347,3.60584160863805));
#52351=CARTESIAN_POINT('Ctrl Pts',(15.1,0.413065612826793,3.5973533346642));
#52352=CARTESIAN_POINT('Ctrl Pts',(15.1,0.400188909388694,3.57223622128044));
#52353=CARTESIAN_POINT('Ctrl Pts',(15.1,0.385429835973237,3.54813135585314));
#52354=CARTESIAN_POINT('Ctrl Pts',(15.1,0.369010648251791,3.52520488756047));
#52355=CARTESIAN_POINT('Ctrl Pts',(15.1,0.352591460530346,3.50227841926781));
#52356=CARTESIAN_POINT('Ctrl Pts',(15.1,0.334512091502091,3.48052876229398));
#52357=CARTESIAN_POINT('Ctrl Pts',(15.1,0.31493781544227,3.46010549098216));
#52358=CARTESIAN_POINT('Ctrl Pts',(14.8800042915148,-1.01702808208336E-5,
4.45785711824254));
#52359=CARTESIAN_POINT('Ctrl Pts',(14.8824938458936,-0.0238866377941533,
4.45787702641871));
#52360=CARTESIAN_POINT('Ctrl Pts',(14.8849834002724,-0.0477600743578134,
4.45604121816599));
#52361=CARTESIAN_POINT('Ctrl Pts',(14.8874729546512,-0.0713366221418418,
4.45232291776013));
#52362=CARTESIAN_POINT('Ctrl Pts',(14.8953443267012,-0.145879994579315,
4.44056654636394));
#52363=CARTESIAN_POINT('Ctrl Pts',(14.9032156987511,-0.217455452203791,
4.40999142286264));
#52364=CARTESIAN_POINT('Ctrl Pts',(14.9110870708011,-0.277486158769077,
4.36426138680722));
#52365=CARTESIAN_POINT('Ctrl Pts',(14.918958442851,-0.337516865334364,4.31853135075179));
#52366=CARTESIAN_POINT('Ctrl Pts',(14.926829814901,-0.38600282084046,4.25764640214225));
#52367=CARTESIAN_POINT('Ctrl Pts',(14.9347011869509,-0.417134151141141,
4.18890214416703));
#52368=CARTESIAN_POINT('Ctrl Pts',(14.9425725590009,-0.448265481441821,
4.12015788619182));
#52369=CARTESIAN_POINT('Ctrl Pts',(14.9504439310508,-0.462042186537087,
4.04355431885095));
#52370=CARTESIAN_POINT('Ctrl Pts',(14.9583153031008,-0.456813159708701,
3.96827104766458));
#52371=CARTESIAN_POINT('Ctrl Pts',(14.9661866751508,-0.451584132880315,
3.89298777647821));
#52372=CARTESIAN_POINT('Ctrl Pts',(14.9740580472007,-0.427349374128277,
3.81902480144635));
#52373=CARTESIAN_POINT('Ctrl Pts',(14.9819294192507,-0.387013471142241,
3.7552443159279));
#52374=CARTESIAN_POINT('Ctrl Pts',(14.9898007913006,-0.346677568156205,
3.69146383040944));
#52375=CARTESIAN_POINT('Ctrl Pts',(14.9976721633506,-0.290240520936171,
3.63786583440439));
#52376=CARTESIAN_POINT('Ctrl Pts',(15.0055435354005,-0.224463896228013,
3.60087434715852));
#52377=CARTESIAN_POINT('Ctrl Pts',(15.0134149074505,-0.158687271519854,
3.56388285991266));
#52378=CARTESIAN_POINT('Ctrl Pts',(15.0212862795004,-0.0835710693235713,
3.54349788142598));
#52379=CARTESIAN_POINT('Ctrl Pts',(15.0291576515504,-0.00811907658734153,
3.54215900695692));
#52380=CARTESIAN_POINT('Ctrl Pts',(15.0370290236004,0.067332916148885,3.54082013248786));
#52381=CARTESIAN_POINT('Ctrl Pts',(15.0449003956503,0.143120699425059,3.55852736203643));
#52382=CARTESIAN_POINT('Ctrl Pts',(15.0527717677003,0.210167800325704,3.59316557823286));
#52383=CARTESIAN_POINT('Ctrl Pts',(15.0606431397502,0.27721490122635,3.62780379442929));
#52384=CARTESIAN_POINT('Ctrl Pts',(15.0685145118002,0.335521319751467,3.67937299727358));
#52385=CARTESIAN_POINT('Ctrl Pts',(15.0763858838501,0.378083948355844,3.74167908197646));
#52386=CARTESIAN_POINT('Ctrl Pts',(15.0842572559001,0.420646576960222,3.80398516667934));
#52387=CARTESIAN_POINT('Ctrl Pts',(15.09212862795,0.447465415643859,3.87702813324079));
#52388=CARTESIAN_POINT('Ctrl Pts',(15.1,0.455362409197302,3.95209810113337));
#52389=CARTESIAN_POINT('Ctrl Pts',(12.5,0.310062960217722,4.54266560670548));
#52390=CARTESIAN_POINT('Ctrl Pts',(12.5,0.283442099593322,4.54921865641189));
#52391=CARTESIAN_POINT('Ctrl Pts',(12.5,0.256466577744696,4.55390832200786));
#52392=CARTESIAN_POINT('Ctrl Pts',(12.5,0.229324391633413,4.55669460918752));
#52393=CARTESIAN_POINT('Ctrl Pts',(12.5,0.202804350211112,4.55941702996513));
#52394=CARTESIAN_POINT('Ctrl Pts',(12.5,0.176124140498118,4.56032157710196));
#52395=CARTESIAN_POINT('Ctrl Pts',(12.5,0.149491279718871,4.55933465732487));
#52396=CARTESIAN_POINT('Ctrl Pts',(12.5,0.131604301980395,4.55867182909064));
#52397=CARTESIAN_POINT('Ctrl Pts',(12.5,0.113739373486447,4.5571550748263));
#52398=CARTESIAN_POINT('Ctrl Pts',(12.5,0.0959711573489174,4.5547553284502));
#52399=CARTESIAN_POINT('Ctrl Pts',(12.5,0.0885102514788159,4.55374767063663));
#52400=CARTESIAN_POINT('Ctrl Pts',(12.5,0.0810658284660142,4.55258395860043));
#52401=CARTESIAN_POINT('Ctrl Pts',(12.5,0.0736590895785168,4.55126509319275));
#52402=CARTESIAN_POINT('Ctrl Pts',(12.5,0.0532014046082737,4.54762233847462));
#52403=CARTESIAN_POINT('Ctrl Pts',(12.5,0.0329999615976937,4.54279338637244));
#52404=CARTESIAN_POINT('Ctrl Pts',(12.5,0.0131662989716721,4.53674486487483));
#52405=CARTESIAN_POINT('Ctrl Pts',(12.5,-0.00550403753485725,4.53105111411095));
#52406=CARTESIAN_POINT('Ctrl Pts',(12.5,-0.0238485481480196,4.52427602479051));
#52407=CARTESIAN_POINT('Ctrl Pts',(12.5,-0.0417515783368052,4.51643454453567));
#52408=CARTESIAN_POINT('Ctrl Pts',(12.5,-0.0500477299146631,4.51280085190917));
#52409=CARTESIAN_POINT('Ctrl Pts',(12.5,-0.058248775177811,4.50893813195896));
#52410=CARTESIAN_POINT('Ctrl Pts',(12.5,-0.0663415323109863,4.50484786558969));
#52411=CARTESIAN_POINT('Ctrl Pts',(12.5,-0.0727048112135971,4.50163171746301));
#52412=CARTESIAN_POINT('Ctrl Pts',(12.5,-0.0789919703630761,4.49827952355299));
#52413=CARTESIAN_POINT('Ctrl Pts',(12.5,-0.085197598682301,4.4947927546146));
#52414=CARTESIAN_POINT('Ctrl Pts',(12.5,-0.104491803581693,4.48395188067351));
#52415=CARTESIAN_POINT('Ctrl Pts',(12.5,-0.123002674071495,4.47180959856144));
#52416=CARTESIAN_POINT('Ctrl Pts',(12.5,-0.140547257611399,4.45840101528927));
#52417=CARTESIAN_POINT('Ctrl Pts',(12.5,-0.156644205929787,4.44609879839914));
#52418=CARTESIAN_POINT('Ctrl Pts',(12.5,-0.17192740174072,4.43272977950413));
#52419=CARTESIAN_POINT('Ctrl Pts',(12.5,-0.186217277007305,4.41832740439832));
#52420=CARTESIAN_POINT('Origin',(15.1,0.,4.));
#52421=CARTESIAN_POINT('',(15.1,-1.16619037896906,2.5));
#52422=CARTESIAN_POINT('',(15.1,1.16619037896906,2.5));
#52423=CARTESIAN_POINT('',(15.1,1.25,2.5));
#52424=CARTESIAN_POINT('Origin',(15.1,0.,4.));
#52425=CARTESIAN_POINT('Origin',(15.1,0.,4.));
#52426=CARTESIAN_POINT('',(15.1,2.75545529808154E-17,5.725));
#52427=CARTESIAN_POINT('Origin',(15.1,0.,5.5));
#52428=CARTESIAN_POINT('',(15.1,1.5,4.225));
#52429=CARTESIAN_POINT('Origin',(15.1,1.5,4.));
#52430=CARTESIAN_POINT('',(15.1,-1.5,4.225));
#52431=CARTESIAN_POINT('Origin',(15.1,-1.5,4.));
#52432=CARTESIAN_POINT('Origin',(14.4,-1.5,4.));
#52433=CARTESIAN_POINT('',(14.5,-1.5,4.225));
#52434=CARTESIAN_POINT('Origin',(14.5,-1.5,4.));
#52435=CARTESIAN_POINT('',(14.4,-1.5,4.225));
#52436=CARTESIAN_POINT('Origin',(14.4,1.5,4.));
#52437=CARTESIAN_POINT('',(14.5,1.5,4.225));
#52438=CARTESIAN_POINT('Origin',(14.5,1.5,4.));
#52439=CARTESIAN_POINT('',(14.4,1.5,4.225));
#52440=CARTESIAN_POINT('Origin',(14.4,0.,5.5));
#52441=CARTESIAN_POINT('',(14.5,-2.75545529808154E-17,5.725));
#52442=CARTESIAN_POINT('Origin',(14.5,0.,5.5));
#52443=CARTESIAN_POINT('',(14.4,-2.75545529808154E-17,5.725));
#52444=CARTESIAN_POINT('Origin',(14.4,2.5,2.5));
#52445=CARTESIAN_POINT('',(14.5,1.16619037896906,2.5));
#52446=CARTESIAN_POINT('',(14.5,-1.16619037896906,2.5));
#52447=CARTESIAN_POINT('',(14.5,1.25,2.5));
#52448=CARTESIAN_POINT('',(14.5,1.16619037896906,2.5));
#52449=CARTESIAN_POINT('',(14.5,-1.16619037896906,2.5));
#52450=CARTESIAN_POINT('Origin',(14.5,0.,4.));
#52451=CARTESIAN_POINT('Origin',(14.5,0.,4.));
#52452=CARTESIAN_POINT('',(14.5,-1.34711147906209E-16,5.1));
#52453=CARTESIAN_POINT('Origin',(14.5,0.,4.));
#52454=CARTESIAN_POINT('Origin',(14.5,0.,4.));
#52455=CARTESIAN_POINT('Origin',(12.5,0.,4.));
#52456=CARTESIAN_POINT('Origin',(12.5,0.,4.));
#52457=CARTESIAN_POINT('',(12.5,-1.34711147906209E-16,5.1));
#52458=CARTESIAN_POINT('',(12.5,-1.34711147906209E-16,5.1));
#52459=CARTESIAN_POINT('Origin',(12.5,0.,4.));
#52460=CARTESIAN_POINT('Origin',(12.5,0.,4.));
#62871=UNCERTAINTY_MEASURE_WITH_UNIT(LENGTH_MEASURE(0.001),#62985,
'DISTANCE_ACCURACY_VALUE',
'Maximum model space distance between geometric entities at asserted c
onnectivities');
#62885=UNCERTAINTY_MEASURE_WITH_UNIT(LENGTH_MEASURE(0.001),#62985,
'DISTANCE_ACCURACY_VALUE',
'Maximum model space distance between geometric entities at asserted c
onnectivities');
#62970=(
GEOMETRIC_REPRESENTATION_CONTEXT(3)
GLOBAL_UNCERTAINTY_ASSIGNED_CONTEXT((#62871))
GLOBAL_UNIT_ASSIGNED_CONTEXT((#62985,#62987,#62988))
REPRESENTATION_CONTEXT('','3D')
);
#62984=(
GEOMETRIC_REPRESENTATION_CONTEXT(3)
GLOBAL_UNCERTAINTY_ASSIGNED_CONTEXT((#62885))
GLOBAL_UNIT_ASSIGNED_CONTEXT((#62985,#62987,#62988))
REPRESENTATION_CONTEXT('','3D')
);
#62985=(
LENGTH_UNIT()
NAMED_UNIT(*)
SI_UNIT(.CENTI.,.METRE.)
);
#62987=(
NAMED_UNIT(*)
PLANE_ANGLE_UNIT()
SI_UNIT($,.RADIAN.)
);
#62988=(
NAMED_UNIT(*)
SI_UNIT($,.STERADIAN.)
SOLID_ANGLE_UNIT()
);
#63073=SHAPE_DEFINITION_REPRESENTATION(#63264,#63433);
#63264=PRODUCT_DEFINITION_SHAPE('',$,#63532);
#63433=SHAPE_REPRESENTATION('',(#26009),#62970);
#63447=PRODUCT_DEFINITION_CONTEXT('part definition',#63743,'design');
#63532=PRODUCT_DEFINITION('Flanged lead nut (1)','Flanged lead nut (1)',#63630,
#63447);
#63630=PRODUCT_DEFINITION_FORMATION('',$,#63829);
#63743=APPLICATION_CONTEXT(
'Core Data for Automotive Mechanical Design Process');
#63744=PRODUCT_CONTEXT('part definition',#63743,'mechanical');
#63829=PRODUCT('Flanged lead nut (1)','Flanged lead nut (1)',
'Flanged lead nut (1)',(#63744));
#63913=COLOUR_RGB('Black',0.12,0.14,0.17);
#63914=FILL_AREA_STYLE_COLOUR('',#63913);
#63915=FILL_AREA_STYLE('',(#63914));
#63916=SURFACE_STYLE_FILL_AREA(#63915);
#63917=SURFACE_SIDE_STYLE('',(#63916));
#63918=SURFACE_STYLE_USAGE(.BOTH.,#63917);
#63919=PRESENTATION_STYLE_ASSIGNMENT((#63918));
ENDSEC;
END-ISO-10303-21;
